ISO-10303-21;
HEADER;
/* Generated by software containing ST-Developer
 * from STEP Tools, Inc. (www.steptools.com) 
 */

FILE_DESCRIPTION(
/* description */ (''),
/* implementation_level */ '2;1');

FILE_NAME(
/* name */ 'Hex nut M3.step',
/* time_stamp */ '2026-11-10T05:20:16-08:00',
/* author */ (''),
/* organization */ (''),
/* preprocessor_version */ 'ST-DEVELOPER v20.2',
/* originating_system */ 'Autodesk Translation Framework v15.17.0.0',
/* authorisation */ '');

FILE_SCHEMA (('AUTOMOTIVE_DESIGN { 1 0 10303 214 3 1 1 }'));
ENDSEC;

DATA;
#10=MECHANICAL_DESIGN_GEOMETRIC_PRESENTATION_REPRESENTATION('',(#119),#24809);
#99=SHAPE_REPRESENTATION_RELATIONSHIP('SRR','None',#24863,#109);
#109=ADVANCED_BREP_SHAPE_REPRESENTATION('',(#129),#24806);
#119=STYLED_ITEM('',(#24923),#129);
#129=MANIFOLD_SOLID_BREP('Body1',#9896);
#183=FACE_BOUND('',#2419,.T.);
#184=FACE_BOUND('',#2428,.T.);
#271=B_SPLINE_SURFACE_WITH_KNOTS('',3,3,((#23593,#23594,#23595,#23596,#23597,
#23598,#23599,#23600,#23601,#23602,#23603,#23604,#23605,#23606,#23607,#23608,
#23609,#23610,#23611,#23612,#23613,#23614,#23615,#23616,#23617,#23618,#23619,
#23620,#23621,#23622,#23623,#23624,#23625,#23626,#23627,#23628),(#23629,
#23630,#23631,#23632,#23633,#23634,#23635,#23636,#23637,#23638,#23639,#23640,
#23641,#23642,#23643,#23644,#23645,#23646,#23647,#23648,#23649,#23650,#23651,
#23652,#23653,#23654,#23655,#23656,#23657,#23658,#23659,#23660,#23661,#23662,
#23663,#23664),(#23665,#23666,#23667,#23668,#23669,#23670,#23671,#23672,
#23673,#23674,#23675,#23676,#23677,#23678,#23679,#23680,#23681,#23682,#23683,
#23684,#23685,#23686,#23687,#23688,#23689,#23690,#23691,#23692,#23693,#23694,
#23695,#23696,#23697,#23698,#23699,#23700),(#23701,#23702,#23703,#23704,
#23705,#23706,#23707,#23708,#23709,#23710,#23711,#23712,#23713,#23714,#23715,
#23716,#23717,#23718,#23719,#23720,#23721,#23722,#23723,#23724,#23725,#23726,
#23727,#23728,#23729,#23730,#23731,#23732,#23733,#23734,#23735,#23736)),
 .UNSPECIFIED.,.F.,.F.,.F.,(4,4),(4,1,1,1,1,1,1,1,1,1,1,1,1,1,1,1,1,1,1,
1,1,1,1,1,1,1,1,1,1,1,1,1,1,4),(0.,0.0321584099938622),(11.8553612635794,
12.830508595889,13.8056559281987,14.7808032605084,15.755950592818,16.7310979251277,
17.7062452574374,18.681392589747,19.6565399220567,20.6316872543664,21.606834586676,
22.5819819189857,23.5571292512954,24.532276583605,25.5074239159147,26.4825712482243,
27.457718580534,28.4328659128437,29.4080132451533,30.383160577463,31.3583079097727,
32.3334552420823,33.308602574392,34.2837499067017,35.2588972390113,36.234044571321,
37.2091919036307,38.1843392359403,39.15948656825,40.1346339005596,41.1097812328693,
42.084928565179,43.0600758974886,44.0352232297983),.UNSPECIFIED.);
#272=B_SPLINE_SURFACE_WITH_KNOTS('',3,3,((#23860,#23861,#23862,#23863,#23864,
#23865,#23866,#23867,#23868,#23869,#23870,#23871,#23872,#23873,#23874,#23875,
#23876,#23877,#23878,#23879,#23880,#23881,#23882,#23883,#23884,#23885,#23886,
#23887,#23888,#23889,#23890,#23891,#23892,#23893,#23894,#23895),(#23896,
#23897,#23898,#23899,#23900,#23901,#23902,#23903,#23904,#23905,#23906,#23907,
#23908,#23909,#23910,#23911,#23912,#23913,#23914,#23915,#23916,#23917,#23918,
#23919,#23920,#23921,#23922,#23923,#23924,#23925,#23926,#23927,#23928,#23929,
#23930,#23931),(#23932,#23933,#23934,#23935,#23936,#23937,#23938,#23939,
#23940,#23941,#23942,#23943,#23944,#23945,#23946,#23947,#23948,#23949,#23950,
#23951,#23952,#23953,#23954,#23955,#23956,#23957,#23958,#23959,#23960,#23961,
#23962,#23963,#23964,#23965,#23966,#23967),(#23968,#23969,#23970,#23971,
#23972,#23973,#23974,#23975,#23976,#23977,#23978,#23979,#23980,#23981,#23982,
#23983,#23984,#23985,#23986,#23987,#23988,#23989,#23990,#23991,#23992,#23993,
#23994,#23995,#23996,#23997,#23998,#23999,#24000,#24001,#24002,#24003)),
 .UNSPECIFIED.,.F.,.F.,.F.,(4,4),(4,1,1,1,1,1,1,1,1,1,1,1,1,1,1,1,1,1,1,
1,1,1,1,1,1,1,1,1,1,1,1,1,1,4),(0.,0.0321584099938622),(14.3984001269719,
15.3735474592815,16.3486947915912,17.3238421239009,18.2989894562105,19.2741367885202,
20.2492841208299,21.2244314531395,22.1995787854492,23.1747261177589,24.1498734500685,
25.1250207823782,26.1001681146879,27.0753154469975,28.0504627793072,29.0256101116168,
30.0007574439265,30.9759047762362,31.9510521085458,32.9261994408555,33.9013467731652,
34.8764941054748,35.8516414377845,36.8267887700942,37.8019361024038,38.7770834347135,
39.7522307670232,40.7273780993328,41.7025254316425,42.6776727639522,43.6528200962618,
44.6279674285715,45.6031147608811,46.5782620931908),.UNSPECIFIED.);
#946=B_SPLINE_CURVE_WITH_KNOTS('',3,(#23263,#23264,#23265,#23266,#23267,
#23268,#23269),.UNSPECIFIED.,.F.,.F.,(4,3,4),(-30.159289474462,-29.2544199692899,
-28.9853432330879),.UNSPECIFIED.);
#947=B_SPLINE_CURVE_WITH_KNOTS('',3,(#23275,#23276,#23277,#23278,#23279,
#23280,#23281,#23282,#23283,#23284,#23285,#23286,#23287,#23288,#23289,#23290,
#23291,#23292,#23293),.UNSPECIFIED.,.F.,.F.,(4,3,3,3,3,3,4),(26.4423043696954,
27.3041253046706,28.2792726369803,29.25441996929,30.2295673015996,31.2047146339093,
32.179861966219),.UNSPECIFIED.);
#948=B_SPLINE_CURVE_WITH_KNOTS('',3,(#23295,#23296,#23297,#23298,#23299,
#23300,#23301,#23302,#23303,#23304,#23305,#23306,#23307,#23308,#23309,#23310,
#23311,#23312,#23313,#23314,#23315,#23316),.UNSPECIFIED.,.F.,.F.,(4,3,3,
3,3,3,3,4),(-28.9853432330879,-28.2792726369803,-27.3041253046706,-26.3289779723609,
-25.3538306400513,-24.3786833077416,-23.403535975432,-22.7021579259084),
 .UNSPECIFIED.);
#949=B_SPLINE_CURVE_WITH_KNOTS('',3,(#23321,#23322,#23323,#23324,#23325,
#23326,#23327,#23328,#23329,#23330,#23331,#23332,#23333,#23334,#23335,#23336,
#23337,#23338,#23339,#23340,#23341,#23342,#23343,#23344,#23345),
 .UNSPECIFIED.,.F.,.F.,(4,3,3,3,3,3,3,3,4),(20.1591190625159,20.478093978503,
21.4532413108126,22.4283886431223,23.403535975432,24.3786833077416,25.3538306400513,
26.328977972361,26.4423043696954),.UNSPECIFIED.);
#950=B_SPLINE_CURVE_WITH_KNOTS('',3,(#23346,#23347,#23348,#23349,#23350,
#23351,#23352,#23353,#23354,#23355,#23356,#23357,#23358,#23359,#23360,#23361,
#23362,#23363,#23364,#23365,#23366,#23367,#23368,#23369,#23370),
 .UNSPECIFIED.,.F.,.F.,(4,3,3,3,3,3,3,3,4),(-22.7021579259084,-22.4283886431223,
-21.4532413108126,-20.478093978503,-19.5029466461933,-18.5277993138836,
-17.552651981574,-16.5775046492643,-16.4189726187288),.UNSPECIFIED.);
#951=B_SPLINE_CURVE_WITH_KNOTS('',3,(#23375,#23376,#23377,#23378,#23379,
#23380,#23381,#23382,#23383,#23384,#23385,#23386,#23387,#23388,#23389,#23390,
#23391,#23392,#23393,#23394,#23395,#23396),.UNSPECIFIED.,.F.,.F.,(4,3,3,
3,3,3,3,4),(13.8759337553363,14.627209984645,15.6023573169546,16.5775046492643,
17.552651981574,18.5277993138836,19.5029466461933,20.1591190625159),
 .UNSPECIFIED.);
#952=B_SPLINE_CURVE_WITH_KNOTS('',3,(#23397,#23398,#23399,#23400,#23401,
#23402,#23403,#23404,#23405,#23406,#23407,#23408,#23409,#23410,#23411,#23412,
#23413,#23414,#23415,#23416,#23417,#23418),.UNSPECIFIED.,.F.,.F.,(4,3,3,
3,3,3,3,4),(-16.4189726187288,-15.6023573169546,-14.627209984645,-13.6520626523353,
-12.6769153200256,-11.701767987716,-10.7266206554063,-10.1357873115492),
 .UNSPECIFIED.);
#953=B_SPLINE_CURVE_WITH_KNOTS('',3,(#23424,#23425,#23426,#23427,#23428,
#23429,#23430,#23431,#23432,#23433,#23434,#23435,#23436),.UNSPECIFIED.,
 .F.,.F.,(4,3,3,3,4),(-3.8526020043696,-2.92544199692899,-1.95029466461933,
-0.975147332309664,0.),.UNSPECIFIED.);
#954=B_SPLINE_CURVE_WITH_KNOTS('',3,(#23439,#23440,#23441,#23442,#23443,
#23444,#23445,#23446,#23447,#23448,#23449,#23450,#23451,#23452,#23453,#23454,
#23455,#23456,#23457),.UNSPECIFIED.,.F.,.F.,(4,3,3,3,3,3,4),(2.02057249175693,
2.925441996929,3.90058932923866,4.87573666154832,5.85088399385799,6.82603132616766,
7.59274844815668),.UNSPECIFIED.);
#955=B_SPLINE_CURVE_WITH_KNOTS('',3,(#23463,#23464,#23465,#23466,#23467,
#23468,#23469),.UNSPECIFIED.,.F.,.F.,(4,1,1,1,4),(40.8407044966673,41.1097812328693,
42.084928565179,43.0600758974886,44.0352232297983),.UNSPECIFIED.);
#956=B_SPLINE_CURVE_WITH_KNOTS('',3,(#23472,#23473,#23474,#23475,#23476,
#23477,#23478),.UNSPECIFIED.,.F.,.F.,(4,1,1,1,4),(40.8407044966673,41.7025254316425,
42.6776727639522,43.6528200962618,44.5576896014339),.UNSPECIFIED.);
#957=B_SPLINE_CURVE_WITH_KNOTS('',3,(#23483,#23484,#23485,#23486,#23487,
#23488,#23489,#23490,#23491,#23492),.UNSPECIFIED.,.F.,.F.,(4,1,1,1,1,1,
1,4),(34.5575191894877,35.2588972390113,36.234044571321,37.2091919036307,
38.1843392359403,39.15948656825,40.1346339005596,40.8407044966673),
 .UNSPECIFIED.);
#958=B_SPLINE_CURVE_WITH_KNOTS('',3,(#23493,#23494,#23495,#23496,#23497,
#23498,#23499,#23500,#23501,#23502,#23503),.UNSPECIFIED.,.F.,.F.,(4,1,1,
1,1,1,1,1,4),(34.5575191894877,34.8764941054748,35.8516414377845,36.8267887700942,
37.8019361024038,38.7770834347135,39.7522307670232,40.7273780993328,40.8407044966673),
 .UNSPECIFIED.);
#959=B_SPLINE_CURVE_WITH_KNOTS('',3,(#23508,#23509,#23510,#23511,#23512,
#23513,#23514,#23515,#23516,#23517,#23518),.UNSPECIFIED.,.F.,.F.,(4,1,1,
1,1,1,1,1,4),(28.2743338823081,28.4328659128437,29.4080132451533,30.383160577463,
31.3583079097727,32.3334552420823,33.308602574392,34.2837499067017,34.5575191894877),
 .UNSPECIFIED.);
#960=B_SPLINE_CURVE_WITH_KNOTS('',3,(#23519,#23520,#23521,#23522,#23523,
#23524,#23525,#23526,#23527,#23528),.UNSPECIFIED.,.F.,.F.,(4,1,1,1,1,1,
1,4),(28.2743338823081,29.0256101116168,30.0007574439265,30.9759047762362,
31.9510521085458,32.9261994408555,33.9013467731652,34.5575191894877),
 .UNSPECIFIED.);
#961=B_SPLINE_CURVE_WITH_KNOTS('',3,(#23533,#23534,#23535,#23536,#23537,
#23538,#23539,#23540,#23541,#23542),.UNSPECIFIED.,.F.,.F.,(4,1,1,1,1,1,
1,4),(21.9911485751285,22.5819819189857,23.5571292512954,24.532276583605,
25.5074239159147,26.4825712482243,27.457718580534,28.2743338823081),
 .UNSPECIFIED.);
#962=B_SPLINE_CURVE_WITH_KNOTS('',3,(#23543,#23544,#23545,#23546,#23547,
#23548,#23549,#23550,#23551,#23552,#23553),.UNSPECIFIED.,.F.,.F.,(4,1,1,
1,1,1,1,1,4),(21.9911485751285,22.1995787854492,23.1747261177589,24.1498734500685,
25.1250207823782,26.1001681146879,27.0753154469975,28.0504627793072,28.2743338823081),
 .UNSPECIFIED.);
#963=B_SPLINE_CURVE_WITH_KNOTS('',3,(#23559,#23560,#23561,#23562,#23563),
 .UNSPECIFIED.,.F.,.F.,(4,1,4),(14.3984001269719,15.3735474592815,15.7079632679489),
 .UNSPECIFIED.);
#964=B_SPLINE_CURVE_WITH_KNOTS('',3,(#23566,#23567,#23568,#23569,#23570),
 .UNSPECIFIED.,.F.,.F.,(4,1,4),(13.8759337553363,14.7808032605084,15.7079632679489),
 .UNSPECIFIED.);
#965=B_SPLINE_CURVE_WITH_KNOTS('',3,(#23572,#23573,#23574,#23575,#23576,
#23577,#23578,#23579,#23580,#23581,#23582),.UNSPECIFIED.,.F.,.F.,(4,1,1,
1,1,1,1,1,4),(15.7079632679489,15.755950592818,16.7310979251277,17.7062452574374,
18.681392589747,19.6565399220567,20.6316872543664,21.606834586676,21.9911485751285),
 .UNSPECIFIED.);
#966=B_SPLINE_CURVE_WITH_KNOTS('',3,(#23583,#23584,#23585,#23586,#23587,
#23588,#23589,#23590,#23591,#23592),.UNSPECIFIED.,.F.,.F.,(4,1,1,1,1,1,
1,4),(15.7079632679489,16.3486947915912,17.3238421239009,18.2989894562105,
19.2741367885202,20.2492841208299,21.2244314531395,21.9911485751285),
 .UNSPECIFIED.);
#967=B_SPLINE_CURVE_WITH_KNOTS('',3,(#23737,#23738,#23739,#23740,#23741,
#23742,#23743,#23744,#23745,#23746,#23747,#23748,#23749,#23750,#23751,#23752,
#23753,#23754,#23755,#23756,#23757,#23758,#23759,#23760,#23761,#23762,#23763,
#23764,#23765,#23766,#23767,#23768,#23769,#23770,#23771,#23772,#23773,#23774,
#23775,#23776,#23777,#23778,#23779,#23780,#23781,#23782,#23783,#23784,#23785),
 .UNSPECIFIED.,.F.,.F.,(4,3,3,3,3,3,3,3,3,3,3,3,3,3,3,3,4),(0.,0.0320333804888866,
0.0505515708593653,0.0603413132804416,0.0917900141854983,0.108096115778005,
0.122914675479851,0.145143248337739,0.168151513577436,0.177516949333476,
0.202471322707608,0.21794283081622,0.231200110368267,0.247503117401854,
0.263651632124391,0.277334442830003,0.286347380332244),.UNSPECIFIED.);
#968=B_SPLINE_CURVE_WITH_KNOTS('',3,(#23786,#23787,#23788,#23789,#23790,
#23791,#23792,#23793,#23794,#23795,#23796,#23797,#23798,#23799,#23800,#23801,
#23802,#23803,#23804,#23805,#23806,#23807,#23808,#23809,#23810,#23811,#23812,
#23813,#23814,#23815,#23816,#23817,#23818,#23819,#23820,#23821,#23822,#23823,
#23824,#23825,#23826,#23827,#23828,#23829,#23830,#23831,#23832,#23833,#23834),
 .UNSPECIFIED.,.F.,.F.,(4,3,3,3,3,3,3,3,3,3,3,3,3,3,3,3,4),(0.,0.0274305464075637,
0.0492901149097146,0.0591933555873536,0.0887250095166089,0.100015570674795,
0.108381796308415,0.130826479038955,0.152531076563578,0.162815893631175,
0.190691958353668,0.212372986031639,0.222945305605857,0.245534254906135,
0.257847836118801,0.274320152521146,0.28514280399515),.UNSPECIFIED.);
#969=B_SPLINE_CURVE_WITH_KNOTS('',3,(#23835,#23836,#23837,#23838,#23839,
#23840,#23841,#23842,#23843,#23844,#23845,#23846,#23847,#23848,#23849,#23850,
#23851,#23852,#23853,#23854,#23855,#23856,#23857,#23858,#23859),
 .UNSPECIFIED.,.F.,.F.,(4,3,3,3,3,3,3,3,4),(-10.1357873115492,-9.75147332309665,
-8.77632599078699,-7.80117865847732,-6.82603132616766,-5.85088399385799,
-4.87573666154833,-3.90058932923866,-3.8526020043696),.UNSPECIFIED.);
#970=B_SPLINE_CURVE_WITH_KNOTS('',3,(#24004,#24005,#24006,#24007,#24008,
#24009,#24010,#24011,#24012,#24013,#24014,#24015,#24016,#24017,#24018,#24019,
#24020,#24021,#24022,#24023,#24024,#24025,#24026,#24027,#24028,#24029,#24030,
#24031,#24032,#24033,#24034,#24035,#24036,#24037,#24038,#24039,#24040,#24041,
#24042,#24043,#24044,#24045,#24046,#24047,#24048,#24049,#24050,#24051,#24052),
 .UNSPECIFIED.,.F.,.F.,(4,3,3,3,3,3,3,3,3,3,3,3,3,3,3,3,4),(0.,0.0274305890506951,
0.0492901290331875,0.0591933603491513,0.0887250177779717,0.100015607166709,
0.108381835831352,0.13082647903896,0.152531071764912,0.162815892251191,
0.190691957318683,0.212372984486691,0.22294529735758,0.245534140364172,
0.257847701250626,0.274320152521159,0.285142803995162),.UNSPECIFIED.);
#971=B_SPLINE_CURVE_WITH_KNOTS('',3,(#24053,#24054,#24055,#24056,#24057,
#24058,#24059,#24060,#24061,#24062,#24063,#24064,#24065,#24066,#24067,#24068,
#24069,#24070,#24071,#24072,#24073,#24074,#24075,#24076,#24077),
 .UNSPECIFIED.,.F.,.F.,(4,3,3,3,3,3,3,3,4),(7.59274844815668,7.80117865847732,
8.77632599078698,9.75147332309665,10.7266206554063,11.701767987716,12.6769153200256,
13.6520626523353,13.8759337553363),.UNSPECIFIED.);
#972=B_SPLINE_CURVE_WITH_KNOTS('',3,(#24078,#24079,#24080,#24081,#24082,
#24083,#24084,#24085,#24086,#24087,#24088,#24089,#24090,#24091,#24092,#24093,
#24094,#24095,#24096,#24097,#24098,#24099,#24100,#24101,#24102,#24103,#24104,
#24105,#24106,#24107,#24108,#24109,#24110,#24111,#24112,#24113,#24114,#24115,
#24116,#24117,#24118,#24119,#24120,#24121,#24122,#24123,#24124,#24125,#24126),
 .UNSPECIFIED.,.F.,.F.,(4,3,3,3,3,3,3,3,3,3,3,3,3,3,3,3,4),(0.,0.0320334058164849,
0.0505515938322513,0.0603413311462071,0.0917900214840119,0.108096111687201,
0.122914678304232,0.145143248337743,0.168151527562726,0.177516955081398,
0.202471327018552,0.217942288122009,0.231200024743484,0.24750284136614,
0.263651600306541,0.277334442830014,0.286347380332252),.UNSPECIFIED.);
#1288=PLANE('',#10586);
#1289=PLANE('',#10588);
#1290=PLANE('',#10589);
#1291=PLANE('',#10590);
#1292=PLANE('',#10591);
#1293=PLANE('',#10592);
#1294=PLANE('',#10593);
#1295=PLANE('',#10594);
#1801=FACE_OUTER_BOUND('',#2405,.T.);
#1802=FACE_OUTER_BOUND('',#2406,.T.);
#1803=FACE_OUTER_BOUND('',#2407,.T.);
#1804=FACE_OUTER_BOUND('',#2408,.T.);
#1805=FACE_OUTER_BOUND('',#2409,.T.);
#1806=FACE_OUTER_BOUND('',#2410,.T.);
#1807=FACE_OUTER_BOUND('',#2411,.T.);
#1808=FACE_OUTER_BOUND('',#2412,.T.);
#1809=FACE_OUTER_BOUND('',#2413,.T.);
#1810=FACE_OUTER_BOUND('',#2414,.T.);
#1811=FACE_OUTER_BOUND('',#2415,.T.);
#1812=FACE_OUTER_BOUND('',#2416,.T.);
#1813=FACE_OUTER_BOUND('',#2417,.T.);
#1814=FACE_OUTER_BOUND('',#2418,.T.);
#1815=FACE_OUTER_BOUND('',#2420,.T.);
#1816=FACE_OUTER_BOUND('',#2421,.T.);
#1817=FACE_OUTER_BOUND('',#2422,.T.);
#1818=FACE_OUTER_BOUND('',#2423,.T.);
#1819=FACE_OUTER_BOUND('',#2424,.T.);
#1820=FACE_OUTER_BOUND('',#2425,.T.);
#1821=FACE_OUTER_BOUND('',#2426,.T.);
#1822=FACE_OUTER_BOUND('',#2427,.T.);
#2405=EDGE_LOOP('',(#8925,#8926,#8927));
#2406=EDGE_LOOP('',(#8928,#8929,#8930,#8931,#8932));
#2407=EDGE_LOOP('',(#8933,#8934,#8935,#8936));
#2408=EDGE_LOOP('',(#8937,#8938,#8939,#8940));
#2409=EDGE_LOOP('',(#8941,#8942,#8943,#8944));
#2410=EDGE_LOOP('',(#8945,#8946,#8947,#8948));
#2411=EDGE_LOOP('',(#8949,#8950,#8951,#8952));
#2412=EDGE_LOOP('',(#8953,#8954,#8955,#8956));
#2413=EDGE_LOOP('',(#8957,#8958,#8959,#8960));
#2414=EDGE_LOOP('',(#8961,#8962,#8963,#8964));
#2415=EDGE_LOOP('',(#8965,#8966,#8967,#8968));
#2416=EDGE_LOOP('',(#8969,#8970,#8971,#8972,#8973,#8974,#8975,#8976,#8977,
#8978,#8979,#8980,#8981,#8982));
#2417=EDGE_LOOP('',(#8983,#8984,#8985,#8986,#8987,#8988,#8989,#8990,#8991,
#8992,#8993,#8994,#8995));
#2418=EDGE_LOOP('',(#8996,#8997,#8998,#8999,#9000,#9001));
#2419=EDGE_LOOP('',(#9002,#9003,#9004,#9005));
#2420=EDGE_LOOP('',(#9006,#9007,#9008,#9009));
#2421=EDGE_LOOP('',(#9010,#9011,#9012,#9013));
#2422=EDGE_LOOP('',(#9014,#9015,#9016,#9017));
#2423=EDGE_LOOP('',(#9018,#9019,#9020,#9021));
#2424=EDGE_LOOP('',(#9022,#9023,#9024,#9025));
#2425=EDGE_LOOP('',(#9026,#9027,#9028,#9029));
#2426=EDGE_LOOP('',(#9030,#9031,#9032,#9033));
#2427=EDGE_LOOP('',(#9034,#9035,#9036,#9037,#9038,#9039));
#2428=EDGE_LOOP('',(#9040,#9041,#9042,#9043,#9044));
#3025=LINE('',#23260,#3613);
#3026=LINE('',#23273,#3614);
#3027=LINE('',#23320,#3615);
#3028=LINE('',#23374,#3616);
#3029=LINE('',#23422,#3617);
#3030=LINE('',#23461,#3618);
#3031=LINE('',#23482,#3619);
#3032=LINE('',#23507,#3620);
#3033=LINE('',#23532,#3621);
#3034=LINE('',#23557,#3622);
#3035=LINE('',#24130,#3623);
#3036=LINE('',#24132,#3624);
#3037=LINE('',#24134,#3625);
#3038=LINE('',#24136,#3626);
#3039=LINE('',#24138,#3627);
#3040=LINE('',#24139,#3628);
#3041=LINE('',#24144,#3629);
#3042=LINE('',#24145,#3630);
#3043=LINE('',#24146,#3631);
#3044=LINE('',#24149,#3632);
#3045=LINE('',#24150,#3633);
#3046=LINE('',#24153,#3634);
#3047=LINE('',#24154,#3635);
#3048=LINE('',#24157,#3636);
#3049=LINE('',#24158,#3637);
#3050=LINE('',#24161,#3638);
#3051=LINE('',#24162,#3639);
#3052=LINE('',#24164,#3640);
#3613=VECTOR('',#12337,0.15);
#3614=VECTOR('',#12342,0.15);
#3615=VECTOR('',#12347,0.15);
#3616=VECTOR('',#12350,0.15);
#3617=VECTOR('',#12353,0.15);
#3618=VECTOR('',#12358,0.1543);
#3619=VECTOR('',#12363,0.1543);
#3620=VECTOR('',#12366,0.1543);
#3621=VECTOR('',#12369,0.1543);
#3622=VECTOR('',#12372,0.1543);
#3623=VECTOR('',#12379,1.);
#3624=VECTOR('',#12380,1.);
#3625=VECTOR('',#12381,1.);
#3626=VECTOR('',#12382,1.);
#3627=VECTOR('',#12383,1.);
#3628=VECTOR('',#12384,1.);
#3629=VECTOR('',#12389,1.);
#3630=VECTOR('',#12390,1.);
#3631=VECTOR('',#12391,1.);
#3632=VECTOR('',#12394,1.);
#3633=VECTOR('',#12395,1.);
#3634=VECTOR('',#12398,1.);
#3635=VECTOR('',#12399,1.);
#3636=VECTOR('',#12402,1.);
#3637=VECTOR('',#12403,1.);
#3638=VECTOR('',#12406,1.);
#3639=VECTOR('',#12407,1.);
#3640=VECTOR('',#12410,1.);
#3790=CIRCLE('',#10571,0.12645);
#3791=CIRCLE('',#10573,0.12645);
#3792=CIRCLE('',#10577,0.12645);
#3793=CIRCLE('',#10579,0.1543);
#3794=CIRCLE('',#10584,0.1543);
#4699=VERTEX_POINT('',#23258);
#4700=VERTEX_POINT('',#23259);
#4701=VERTEX_POINT('',#23261);
#4702=VERTEX_POINT('',#23271);
#4703=VERTEX_POINT('',#23272);
#4704=VERTEX_POINT('',#23274);
#4705=VERTEX_POINT('',#23318);
#4706=VERTEX_POINT('',#23319);
#4707=VERTEX_POINT('',#23372);
#4708=VERTEX_POINT('',#23373);
#4709=VERTEX_POINT('',#23420);
#4710=VERTEX_POINT('',#23421);
#4711=VERTEX_POINT('',#23423);
#4712=VERTEX_POINT('',#23437);
#4713=VERTEX_POINT('',#23459);
#4714=VERTEX_POINT('',#23460);
#4715=VERTEX_POINT('',#23462);
#4716=VERTEX_POINT('',#23470);
#4717=VERTEX_POINT('',#23480);
#4718=VERTEX_POINT('',#23481);
#4719=VERTEX_POINT('',#23505);
#4720=VERTEX_POINT('',#23506);
#4721=VERTEX_POINT('',#23530);
#4722=VERTEX_POINT('',#23531);
#4723=VERTEX_POINT('',#23555);
#4724=VERTEX_POINT('',#23556);
#4725=VERTEX_POINT('',#23558);
#4726=VERTEX_POINT('',#23564);
#4727=VERTEX_POINT('',#24128);
#4728=VERTEX_POINT('',#24129);
#4729=VERTEX_POINT('',#24131);
#4730=VERTEX_POINT('',#24133);
#4731=VERTEX_POINT('',#24135);
#4732=VERTEX_POINT('',#24137);
#4733=VERTEX_POINT('',#24142);
#4734=VERTEX_POINT('',#24143);
#4735=VERTEX_POINT('',#24148);
#4736=VERTEX_POINT('',#24152);
#4737=VERTEX_POINT('',#24156);
#4738=VERTEX_POINT('',#24160);
#6121=EDGE_CURVE('',#4699,#4700,#3025,.T.);
#6122=EDGE_CURVE('',#4701,#4700,#3790,.F.);
#6123=EDGE_CURVE('',#4701,#4699,#946,.T.);
#6124=EDGE_CURVE('',#4702,#4703,#3026,.T.);
#6125=EDGE_CURVE('',#4703,#4704,#947,.T.);
#6126=EDGE_CURVE('',#4700,#4704,#3791,.F.);
#6127=EDGE_CURVE('',#4699,#4702,#948,.T.);
#6128=EDGE_CURVE('',#4705,#4706,#3027,.T.);
#6129=EDGE_CURVE('',#4706,#4703,#949,.T.);
#6130=EDGE_CURVE('',#4702,#4705,#950,.T.);
#6131=EDGE_CURVE('',#4707,#4708,#3028,.T.);
#6132=EDGE_CURVE('',#4708,#4706,#951,.T.);
#6133=EDGE_CURVE('',#4705,#4707,#952,.T.);
#6134=EDGE_CURVE('',#4709,#4710,#3029,.T.);
#6135=EDGE_CURVE('',#4709,#4711,#953,.T.);
#6136=EDGE_CURVE('',#4712,#4711,#3792,.T.);
#6137=EDGE_CURVE('',#4712,#4710,#954,.T.);
#6138=EDGE_CURVE('',#4713,#4714,#3030,.T.);
#6139=EDGE_CURVE('',#4714,#4715,#955,.T.);
#6140=EDGE_CURVE('',#4716,#4715,#3793,.T.);
#6141=EDGE_CURVE('',#4713,#4716,#956,.T.);
#6142=EDGE_CURVE('',#4717,#4718,#3031,.T.);
#6143=EDGE_CURVE('',#4718,#4714,#957,.T.);
#6144=EDGE_CURVE('',#4717,#4713,#958,.T.);
#6145=EDGE_CURVE('',#4719,#4720,#3032,.T.);
#6146=EDGE_CURVE('',#4720,#4718,#959,.T.);
#6147=EDGE_CURVE('',#4719,#4717,#960,.T.);
#6148=EDGE_CURVE('',#4721,#4722,#3033,.T.);
#6149=EDGE_CURVE('',#4722,#4720,#961,.T.);
#6150=EDGE_CURVE('',#4721,#4719,#962,.T.);
#6151=EDGE_CURVE('',#4723,#4724,#3034,.T.);
#6152=EDGE_CURVE('',#4725,#4723,#963,.T.);
#6153=EDGE_CURVE('',#4726,#4725,#3794,.T.);
#6154=EDGE_CURVE('',#4726,#4724,#964,.T.);
#6155=EDGE_CURVE('',#4724,#4722,#965,.T.);
#6156=EDGE_CURVE('',#4723,#4721,#966,.T.);
#6157=EDGE_CURVE('',#4715,#4701,#967,.T.);
#6158=EDGE_CURVE('',#4711,#4726,#968,.T.);
#6159=EDGE_CURVE('',#4707,#4709,#969,.T.);
#6160=EDGE_CURVE('',#4704,#4716,#970,.T.);
#6161=EDGE_CURVE('',#4710,#4708,#971,.T.);
#6162=EDGE_CURVE('',#4725,#4712,#972,.T.);
#6163=EDGE_CURVE('',#4727,#4728,#3035,.T.);
#6164=EDGE_CURVE('',#4728,#4729,#3036,.T.);
#6165=EDGE_CURVE('',#4729,#4730,#3037,.T.);
#6166=EDGE_CURVE('',#4730,#4731,#3038,.T.);
#6167=EDGE_CURVE('',#4731,#4732,#3039,.T.);
#6168=EDGE_CURVE('',#4732,#4727,#3040,.T.);
#6169=EDGE_CURVE('',#4733,#4734,#3041,.T.);
#6170=EDGE_CURVE('',#4734,#4727,#3042,.T.);
#6171=EDGE_CURVE('',#4733,#4732,#3043,.T.);
#6172=EDGE_CURVE('',#4735,#4733,#3044,.T.);
#6173=EDGE_CURVE('',#4735,#4731,#3045,.T.);
#6174=EDGE_CURVE('',#4736,#4735,#3046,.T.);
#6175=EDGE_CURVE('',#4736,#4730,#3047,.T.);
#6176=EDGE_CURVE('',#4737,#4736,#3048,.T.);
#6177=EDGE_CURVE('',#4737,#4729,#3049,.T.);
#6178=EDGE_CURVE('',#4738,#4737,#3050,.T.);
#6179=EDGE_CURVE('',#4738,#4728,#3051,.T.);
#6180=EDGE_CURVE('',#4734,#4738,#3052,.T.);
#8925=ORIENTED_EDGE('',*,*,#6121,.T.);
#8926=ORIENTED_EDGE('',*,*,#6122,.F.);
#8927=ORIENTED_EDGE('',*,*,#6123,.T.);
#8928=ORIENTED_EDGE('',*,*,#6124,.T.);
#8929=ORIENTED_EDGE('',*,*,#6125,.T.);
#8930=ORIENTED_EDGE('',*,*,#6126,.F.);
#8931=ORIENTED_EDGE('',*,*,#6121,.F.);
#8932=ORIENTED_EDGE('',*,*,#6127,.T.);
#8933=ORIENTED_EDGE('',*,*,#6128,.T.);
#8934=ORIENTED_EDGE('',*,*,#6129,.T.);
#8935=ORIENTED_EDGE('',*,*,#6124,.F.);
#8936=ORIENTED_EDGE('',*,*,#6130,.T.);
#8937=ORIENTED_EDGE('',*,*,#6131,.T.);
#8938=ORIENTED_EDGE('',*,*,#6132,.T.);
#8939=ORIENTED_EDGE('',*,*,#6128,.F.);
#8940=ORIENTED_EDGE('',*,*,#6133,.T.);
#8941=ORIENTED_EDGE('',*,*,#6134,.F.);
#8942=ORIENTED_EDGE('',*,*,#6135,.T.);
#8943=ORIENTED_EDGE('',*,*,#6136,.F.);
#8944=ORIENTED_EDGE('',*,*,#6137,.T.);
#8945=ORIENTED_EDGE('',*,*,#6138,.T.);
#8946=ORIENTED_EDGE('',*,*,#6139,.T.);
#8947=ORIENTED_EDGE('',*,*,#6140,.F.);
#8948=ORIENTED_EDGE('',*,*,#6141,.F.);
#8949=ORIENTED_EDGE('',*,*,#6142,.T.);
#8950=ORIENTED_EDGE('',*,*,#6143,.T.);
#8951=ORIENTED_EDGE('',*,*,#6138,.F.);
#8952=ORIENTED_EDGE('',*,*,#6144,.F.);
#8953=ORIENTED_EDGE('',*,*,#6145,.T.);
#8954=ORIENTED_EDGE('',*,*,#6146,.T.);
#8955=ORIENTED_EDGE('',*,*,#6142,.F.);
#8956=ORIENTED_EDGE('',*,*,#6147,.F.);
#8957=ORIENTED_EDGE('',*,*,#6148,.T.);
#8958=ORIENTED_EDGE('',*,*,#6149,.T.);
#8959=ORIENTED_EDGE('',*,*,#6145,.F.);
#8960=ORIENTED_EDGE('',*,*,#6150,.F.);
#8961=ORIENTED_EDGE('',*,*,#6151,.F.);
#8962=ORIENTED_EDGE('',*,*,#6152,.F.);
#8963=ORIENTED_EDGE('',*,*,#6153,.F.);
#8964=ORIENTED_EDGE('',*,*,#6154,.T.);
#8965=ORIENTED_EDGE('',*,*,#6151,.T.);
#8966=ORIENTED_EDGE('',*,*,#6155,.T.);
#8967=ORIENTED_EDGE('',*,*,#6148,.F.);
#8968=ORIENTED_EDGE('',*,*,#6156,.F.);
#8969=ORIENTED_EDGE('',*,*,#6157,.F.);
#8970=ORIENTED_EDGE('',*,*,#6139,.F.);
#8971=ORIENTED_EDGE('',*,*,#6143,.F.);
#8972=ORIENTED_EDGE('',*,*,#6146,.F.);
#8973=ORIENTED_EDGE('',*,*,#6149,.F.);
#8974=ORIENTED_EDGE('',*,*,#6155,.F.);
#8975=ORIENTED_EDGE('',*,*,#6154,.F.);
#8976=ORIENTED_EDGE('',*,*,#6158,.F.);
#8977=ORIENTED_EDGE('',*,*,#6135,.F.);
#8978=ORIENTED_EDGE('',*,*,#6159,.F.);
#8979=ORIENTED_EDGE('',*,*,#6133,.F.);
#8980=ORIENTED_EDGE('',*,*,#6130,.F.);
#8981=ORIENTED_EDGE('',*,*,#6127,.F.);
#8982=ORIENTED_EDGE('',*,*,#6123,.F.);
#8983=ORIENTED_EDGE('',*,*,#6160,.F.);
#8984=ORIENTED_EDGE('',*,*,#6125,.F.);
#8985=ORIENTED_EDGE('',*,*,#6129,.F.);
#8986=ORIENTED_EDGE('',*,*,#6132,.F.);
#8987=ORIENTED_EDGE('',*,*,#6161,.F.);
#8988=ORIENTED_EDGE('',*,*,#6137,.F.);
#8989=ORIENTED_EDGE('',*,*,#6162,.F.);
#8990=ORIENTED_EDGE('',*,*,#6152,.T.);
#8991=ORIENTED_EDGE('',*,*,#6156,.T.);
#8992=ORIENTED_EDGE('',*,*,#6150,.T.);
#8993=ORIENTED_EDGE('',*,*,#6147,.T.);
#8994=ORIENTED_EDGE('',*,*,#6144,.T.);
#8995=ORIENTED_EDGE('',*,*,#6141,.T.);
#8996=ORIENTED_EDGE('',*,*,#6163,.T.);
#8997=ORIENTED_EDGE('',*,*,#6164,.T.);
#8998=ORIENTED_EDGE('',*,*,#6165,.T.);
#8999=ORIENTED_EDGE('',*,*,#6166,.T.);
#9000=ORIENTED_EDGE('',*,*,#6167,.T.);
#9001=ORIENTED_EDGE('',*,*,#6168,.T.);
#9002=ORIENTED_EDGE('',*,*,#6158,.T.);
#9003=ORIENTED_EDGE('',*,*,#6153,.T.);
#9004=ORIENTED_EDGE('',*,*,#6162,.T.);
#9005=ORIENTED_EDGE('',*,*,#6136,.T.);
#9006=ORIENTED_EDGE('',*,*,#6134,.T.);
#9007=ORIENTED_EDGE('',*,*,#6161,.T.);
#9008=ORIENTED_EDGE('',*,*,#6131,.F.);
#9009=ORIENTED_EDGE('',*,*,#6159,.T.);
#9010=ORIENTED_EDGE('',*,*,#6169,.T.);
#9011=ORIENTED_EDGE('',*,*,#6170,.T.);
#9012=ORIENTED_EDGE('',*,*,#6168,.F.);
#9013=ORIENTED_EDGE('',*,*,#6171,.F.);
#9014=ORIENTED_EDGE('',*,*,#6172,.T.);
#9015=ORIENTED_EDGE('',*,*,#6171,.T.);
#9016=ORIENTED_EDGE('',*,*,#6167,.F.);
#9017=ORIENTED_EDGE('',*,*,#6173,.F.);
#9018=ORIENTED_EDGE('',*,*,#6174,.T.);
#9019=ORIENTED_EDGE('',*,*,#6173,.T.);
#9020=ORIENTED_EDGE('',*,*,#6166,.F.);
#9021=ORIENTED_EDGE('',*,*,#6175,.F.);
#9022=ORIENTED_EDGE('',*,*,#6176,.T.);
#9023=ORIENTED_EDGE('',*,*,#6175,.T.);
#9024=ORIENTED_EDGE('',*,*,#6165,.F.);
#9025=ORIENTED_EDGE('',*,*,#6177,.F.);
#9026=ORIENTED_EDGE('',*,*,#6178,.T.);
#9027=ORIENTED_EDGE('',*,*,#6177,.T.);
#9028=ORIENTED_EDGE('',*,*,#6164,.F.);
#9029=ORIENTED_EDGE('',*,*,#6179,.F.);
#9030=ORIENTED_EDGE('',*,*,#6180,.T.);
#9031=ORIENTED_EDGE('',*,*,#6179,.T.);
#9032=ORIENTED_EDGE('',*,*,#6163,.F.);
#9033=ORIENTED_EDGE('',*,*,#6170,.F.);
#9034=ORIENTED_EDGE('',*,*,#6180,.F.);
#9035=ORIENTED_EDGE('',*,*,#6169,.F.);
#9036=ORIENTED_EDGE('',*,*,#6172,.F.);
#9037=ORIENTED_EDGE('',*,*,#6174,.F.);
#9038=ORIENTED_EDGE('',*,*,#6176,.F.);
#9039=ORIENTED_EDGE('',*,*,#6178,.F.);
#9040=ORIENTED_EDGE('',*,*,#6157,.T.);
#9041=ORIENTED_EDGE('',*,*,#6122,.T.);
#9042=ORIENTED_EDGE('',*,*,#6126,.T.);
#9043=ORIENTED_EDGE('',*,*,#6160,.T.);
#9044=ORIENTED_EDGE('',*,*,#6140,.T.);
#9310=CYLINDRICAL_SURFACE('',#10570,0.12645);
#9311=CYLINDRICAL_SURFACE('',#10572,0.12645);
#9312=CYLINDRICAL_SURFACE('',#10574,0.12645);
#9313=CYLINDRICAL_SURFACE('',#10575,0.12645);
#9314=CYLINDRICAL_SURFACE('',#10576,0.12645);
#9315=CYLINDRICAL_SURFACE('',#10578,0.1543);
#9316=CYLINDRICAL_SURFACE('',#10580,0.1543);
#9317=CYLINDRICAL_SURFACE('',#10581,0.1543);
#9318=CYLINDRICAL_SURFACE('',#10582,0.1543);
#9319=CYLINDRICAL_SURFACE('',#10583,0.1543);
#9320=CYLINDRICAL_SURFACE('',#10585,0.1543);
#9321=CYLINDRICAL_SURFACE('',#10587,0.12645);
#9827=ADVANCED_FACE('',(#1801),#9310,.F.);
#9828=ADVANCED_FACE('',(#1802),#9311,.F.);
#9829=ADVANCED_FACE('',(#1803),#9312,.F.);
#9830=ADVANCED_FACE('',(#1804),#9313,.F.);
#9831=ADVANCED_FACE('',(#1805),#9314,.F.);
#9832=ADVANCED_FACE('',(#1806),#9315,.F.);
#9833=ADVANCED_FACE('',(#1807),#9316,.F.);
#9834=ADVANCED_FACE('',(#1808),#9317,.F.);
#9835=ADVANCED_FACE('',(#1809),#9318,.F.);
#9836=ADVANCED_FACE('',(#1810),#9319,.F.);
#9837=ADVANCED_FACE('',(#1811),#9320,.F.);
#9838=ADVANCED_FACE('',(#1812),#271,.F.);
#9839=ADVANCED_FACE('',(#1813),#272,.F.);
#9840=ADVANCED_FACE('',(#1814,#183),#1288,.T.);
#9841=ADVANCED_FACE('',(#1815),#9321,.F.);
#9842=ADVANCED_FACE('',(#1816),#1289,.T.);
#9843=ADVANCED_FACE('',(#1817),#1290,.T.);
#9844=ADVANCED_FACE('',(#1818),#1291,.T.);
#9845=ADVANCED_FACE('',(#1819),#1292,.T.);
#9846=ADVANCED_FACE('',(#1820),#1293,.T.);
#9847=ADVANCED_FACE('',(#1821),#1294,.T.);
#9848=ADVANCED_FACE('',(#1822,#184),#1295,.F.);
#9896=CLOSED_SHELL('',(#9827,#9828,#9829,#9830,#9831,#9832,#9833,#9834,
#9835,#9836,#9837,#9838,#9839,#9840,#9841,#9842,#9843,#9844,#9845,#9846,
#9847,#9848));
#10569=AXIS2_PLACEMENT_3D('',#23256,#12333,#12334);
#10570=AXIS2_PLACEMENT_3D('',#23257,#12335,#12336);
#10571=AXIS2_PLACEMENT_3D('',#23262,#12338,#12339);
#10572=AXIS2_PLACEMENT_3D('',#23270,#12340,#12341);
#10573=AXIS2_PLACEMENT_3D('',#23294,#12343,#12344);
#10574=AXIS2_PLACEMENT_3D('',#23317,#12345,#12346);
#10575=AXIS2_PLACEMENT_3D('',#23371,#12348,#12349);
#10576=AXIS2_PLACEMENT_3D('',#23419,#12351,#12352);
#10577=AXIS2_PLACEMENT_3D('',#23438,#12354,#12355);
#10578=AXIS2_PLACEMENT_3D('',#23458,#12356,#12357);
#10579=AXIS2_PLACEMENT_3D('',#23471,#12359,#12360);
#10580=AXIS2_PLACEMENT_3D('',#23479,#12361,#12362);
#10581=AXIS2_PLACEMENT_3D('',#23504,#12364,#12365);
#10582=AXIS2_PLACEMENT_3D('',#23529,#12367,#12368);
#10583=AXIS2_PLACEMENT_3D('',#23554,#12370,#12371);
#10584=AXIS2_PLACEMENT_3D('',#23565,#12373,#12374);
#10585=AXIS2_PLACEMENT_3D('',#23571,#12375,#12376);
#10586=AXIS2_PLACEMENT_3D('',#24127,#12377,#12378);
#10587=AXIS2_PLACEMENT_3D('',#24140,#12385,#12386);
#10588=AXIS2_PLACEMENT_3D('',#24141,#12387,#12388);
#10589=AXIS2_PLACEMENT_3D('',#24147,#12392,#12393);
#10590=AXIS2_PLACEMENT_3D('',#24151,#12396,#12397);
#10591=AXIS2_PLACEMENT_3D('',#24155,#12400,#12401);
#10592=AXIS2_PLACEMENT_3D('',#24159,#12404,#12405);
#10593=AXIS2_PLACEMENT_3D('',#24163,#12408,#12409);
#10594=AXIS2_PLACEMENT_3D('',#24165,#12411,#12412);
#12333=DIRECTION('axis',(0.,0.,1.));
#12334=DIRECTION('refdir',(1.,0.,0.));
#12335=DIRECTION('center_axis',(0.,0.,-1.));
#12336=DIRECTION('ref_axis',(1.,0.,0.));
#12337=DIRECTION('',(0.,0.,-1.));
#12338=DIRECTION('center_axis',(0.,0.,-1.));
#12339=DIRECTION('ref_axis',(1.,0.,0.));
#12340=DIRECTION('center_axis',(0.,0.,-1.));
#12341=DIRECTION('ref_axis',(1.,0.,0.));
#12342=DIRECTION('',(0.,0.,-1.));
#12343=DIRECTION('center_axis',(0.,0.,-1.));
#12344=DIRECTION('ref_axis',(1.,0.,0.));
#12345=DIRECTION('center_axis',(0.,0.,-1.));
#12346=DIRECTION('ref_axis',(1.,0.,0.));
#12347=DIRECTION('',(0.,0.,-1.));
#12348=DIRECTION('center_axis',(0.,0.,-1.));
#12349=DIRECTION('ref_axis',(1.,0.,0.));
#12350=DIRECTION('',(0.,0.,-1.));
#12351=DIRECTION('center_axis',(0.,0.,-1.));
#12352=DIRECTION('ref_axis',(0.937385399639056,-0.348293859468591,0.));
#12353=DIRECTION('',(0.,0.,-1.));
#12354=DIRECTION('center_axis',(0.,0.,-1.));
#12355=DIRECTION('ref_axis',(1.,0.,0.));
#12356=DIRECTION('center_axis',(0.,0.,-1.));
#12357=DIRECTION('ref_axis',(0.28361887368566,0.958937085782627,0.));
#12358=DIRECTION('',(1.22464679914735E-16,8.07419868282478E-31,-1.));
#12359=DIRECTION('center_axis',(0.,0.,1.));
#12360=DIRECTION('ref_axis',(1.,6.71554824363804E-15,0.));
#12361=DIRECTION('center_axis',(0.,0.,-1.));
#12362=DIRECTION('ref_axis',(1.,6.71554824363804E-15,0.));
#12363=DIRECTION('',(1.22464679914735E-16,8.07419868282478E-31,-1.));
#12364=DIRECTION('center_axis',(0.,0.,-1.));
#12365=DIRECTION('ref_axis',(1.,6.71554824363804E-15,0.));
#12366=DIRECTION('',(1.22464679914735E-16,8.07419868282478E-31,-1.));
#12367=DIRECTION('center_axis',(0.,0.,-1.));
#12368=DIRECTION('ref_axis',(1.,6.71554824363804E-15,0.));
#12369=DIRECTION('',(1.22464679914735E-16,8.07419868282478E-31,-1.));
#12370=DIRECTION('center_axis',(0.,0.,-1.));
#12371=DIRECTION('ref_axis',(-0.60895050335979,-0.793208222636313,0.));
#12372=DIRECTION('',(1.22464679914735E-16,8.07419868282478E-31,-1.));
#12373=DIRECTION('center_axis',(0.,0.,-1.));
#12374=DIRECTION('ref_axis',(1.,6.71554824363804E-15,0.));
#12375=DIRECTION('center_axis',(0.,0.,-1.));
#12376=DIRECTION('ref_axis',(1.,6.71554824363804E-15,0.));
#12377=DIRECTION('center_axis',(0.,0.,1.));
#12378=DIRECTION('ref_axis',(1.,0.,0.));
#12379=DIRECTION('',(0.5,0.866025403784439,0.));
#12380=DIRECTION('',(-0.5,0.866025403784439,0.));
#12381=DIRECTION('',(-1.,0.,0.));
#12382=DIRECTION('',(-0.5,-0.866025403784439,0.));
#12383=DIRECTION('',(0.5,-0.866025403784439,0.));
#12384=DIRECTION('',(1.,-3.49629579342466E-16,0.));
#12385=DIRECTION('center_axis',(0.,0.,-1.));
#12386=DIRECTION('ref_axis',(1.,0.,0.));
#12387=DIRECTION('center_axis',(-3.49629579342466E-16,-1.,0.));
#12388=DIRECTION('ref_axis',(1.,-3.49629579342466E-16,0.));
#12389=DIRECTION('',(1.,-3.49629579342466E-16,0.));
#12390=DIRECTION('',(0.,0.,1.));
#12391=DIRECTION('',(0.,0.,1.));
#12392=DIRECTION('center_axis',(-0.866025403784439,-0.5,0.));
#12393=DIRECTION('ref_axis',(0.5,-0.866025403784439,0.));
#12394=DIRECTION('',(0.5,-0.866025403784439,0.));
#12395=DIRECTION('',(0.,0.,1.));
#12396=DIRECTION('center_axis',(-0.866025403784439,0.5,0.));
#12397=DIRECTION('ref_axis',(-0.5,-0.866025403784439,0.));
#12398=DIRECTION('',(-0.5,-0.866025403784439,0.));
#12399=DIRECTION('',(0.,0.,1.));
#12400=DIRECTION('center_axis',(0.,1.,0.));
#12401=DIRECTION('ref_axis',(-1.,0.,0.));
#12402=DIRECTION('',(-1.,0.,0.));
#12403=DIRECTION('',(0.,0.,1.));
#12404=DIRECTION('center_axis',(0.866025403784439,0.5,0.));
#12405=DIRECTION('ref_axis',(-0.5,0.866025403784439,0.));
#12406=DIRECTION('',(-0.5,0.866025403784439,0.));
#12407=DIRECTION('',(0.,0.,1.));
#12408=DIRECTION('center_axis',(0.866025403784439,-0.5,0.));
#12409=DIRECTION('ref_axis',(0.5,0.866025403784439,0.));
#12410=DIRECTION('',(0.5,0.866025403784439,0.));
#12411=DIRECTION('center_axis',(0.,0.,1.));
#12412=DIRECTION('ref_axis',(1.,0.,0.));
#23256=CARTESIAN_POINT('',(0.,0.,0.));
#23257=CARTESIAN_POINT('Origin',(0.,0.,0.12));
#23258=CARTESIAN_POINT('',(-0.12639138516214,8.91322620741042E-5,0.00934196736194174));
#23259=CARTESIAN_POINT('',(-0.12645,1.54856587752183E-17,-5.55111512312578E-17));
#23260=CARTESIAN_POINT('',(-0.12645,1.54856587752183E-17,0.12));
#23261=CARTESIAN_POINT('',(-0.0488748409397564,0.116622692573588,0.));
#23262=CARTESIAN_POINT('Origin',(0.,0.,0.));
#23263=CARTESIAN_POINT('Ctrl Pts',(-0.0489111879062984,0.116810626195002,
1.20007714660797E-17));
#23264=CARTESIAN_POINT('Ctrl Pts',(-0.0838963038512042,0.101957324585112,
0.00240024091002088));
#23265=CARTESIAN_POINT('Ctrl Pts',(-0.11198221847721,0.0702793053867637,
0.00480048182004174));
#23266=CARTESIAN_POINT('Ctrl Pts',(-0.122072221370749,0.0336561163696377,
0.00720072273006261));
#23267=CARTESIAN_POINT('Ctrl Pts',(-0.125072637487486,0.022765653033531,
0.00791447094068899));
#23268=CARTESIAN_POINT('Ctrl Pts',(-0.126481745582665,0.0114379076904012,
0.00862821915131536));
#23269=CARTESIAN_POINT('Ctrl Pts',(-0.12639138516214,8.91322620741042E-5,
0.00934196736194174));
#23270=CARTESIAN_POINT('Origin',(0.,0.,0.12));
#23271=CARTESIAN_POINT('',(-0.126396145829628,-9.95859796292312E-5,0.0593419673619417));
#23272=CARTESIAN_POINT('',(-0.126575671592806,-7.20628672610732E-5,0.0456580326380584));
#23273=CARTESIAN_POINT('',(-0.12645,1.54856587752183E-17,0.12));
#23274=CARTESIAN_POINT('',(-0.10808967569503,-0.0656218295092665,0.));
#23275=CARTESIAN_POINT('Ctrl Pts',(-0.126575671592806,-7.20628672610732E-5,
0.0456580326380584));
#23276=CARTESIAN_POINT('Ctrl Pts',(-0.126327459688109,0.0361497101693465,
0.0433719816070355));
#23277=CARTESIAN_POINT('Ctrl Pts',(-0.109912066394173,0.0725710138228805,
0.0410859305760125));
#23278=CARTESIAN_POINT('Ctrl Pts',(-0.0824515099939393,0.0961223418729112,
0.0387998795449896));
#23279=CARTESIAN_POINT('Ctrl Pts',(-0.05137998778939,0.122770586059505,
0.036213220908657));
#23280=CARTESIAN_POINT('Ctrl Pts',(-0.00616751748104999,0.132941603485868,
0.0336265622723243));
#23281=CARTESIAN_POINT('Ctrl Pts',(0.0333172074018229,0.122176268745047,
0.0310399036359917));
#23282=CARTESIAN_POINT('Ctrl Pts',(0.0728019322846963,0.111410934004226,
0.028453244999659));
#23283=CARTESIAN_POINT('Ctrl Pts',(0.106558911742102,0.0797092470962188,
0.0258665863633264));
#23284=CARTESIAN_POINT('Ctrl Pts',(0.11981357554495,0.0409763259700822,
0.0232799277269937));
#23285=CARTESIAN_POINT('Ctrl Pts',(0.133068239347797,0.00224340484394604,
0.0206932690906611));
#23286=CARTESIAN_POINT('Ctrl Pts',(0.125820587496086,-0.0435207505003201,
0.0181066104543285));
#23287=CARTESIAN_POINT('Ctrl Pts',(0.101166903546451,-0.0762076816581678,
0.0155199518179958));
#23288=CARTESIAN_POINT('Ctrl Pts',(0.0765132195968157,-0.108894612816016,
0.0129332931816632));
#23289=CARTESIAN_POINT('Ctrl Pts',(0.0344535035492562,-0.128504319787445,
0.0103466345453306));
#23290=CARTESIAN_POINT('Ctrl Pts',(-0.00636464094143544,-0.126469737202777,
0.00775997590899791));
#23291=CARTESIAN_POINT('Ctrl Pts',(-0.0471827854321269,-0.124435154618108,
0.00517331727266527));
#23292=CARTESIAN_POINT('Ctrl Pts',(-0.0867593583659505,-0.100756282477341,
0.00258665863633259));
#23293=CARTESIAN_POINT('Ctrl Pts',(-0.108089675695031,-0.0656218295092657,
-5.55111512312578E-17));
#23294=CARTESIAN_POINT('Origin',(0.,0.,0.));
#23295=CARTESIAN_POINT('Ctrl Pts',(-0.12639138516214,8.91322620741042E-5,
0.00934196736194174));
#23296=CARTESIAN_POINT('Ctrl Pts',(-0.126154274972366,-0.0296906128949183,
0.011214877787648));
#23297=CARTESIAN_POINT('Ctrl Pts',(-0.115592373032178,-0.0596151635265703,
0.0130877882133543));
#23298=CARTESIAN_POINT('Ctrl Pts',(-0.0963650578556872,-0.0821635787359664,
0.0149606986390606));
#23299=CARTESIAN_POINT('Ctrl Pts',(-0.0698103971670931,-0.113304978845907,
0.0175473572753932));
#23300=CARTESIAN_POINT('Ctrl Pts',(-0.0267272342632827,-0.130377059081323,
0.0201340159117258));
#23301=CARTESIAN_POINT('Ctrl Pts',(0.0139574509341311,-0.125868770046104,
0.0227206745480584));
#23302=CARTESIAN_POINT('Ctrl Pts',(0.0546421361315456,-0.121360481010885,
0.0253073331843911));
#23303=CARTESIAN_POINT('Ctrl Pts',(0.0929283436225635,-0.0952718227050311,
0.0278939918207237));
#23304=CARTESIAN_POINT('Ctrl Pts',(0.112018291148455,-0.0590635258734944,
0.0304806504570564));
#23305=CARTESIAN_POINT('Ctrl Pts',(0.131108238674346,-0.0228552290419586,
0.033067309093389));
#23306=CARTESIAN_POINT('Ctrl Pts',(0.131001926235112,0.0234727063152593,
0.0356539677297216));
#23307=CARTESIAN_POINT('Ctrl Pts',(0.111741771403992,0.0595891814911641,
0.0382406263660542));
#23308=CARTESIAN_POINT('Ctrl Pts',(0.0924816165728724,0.0957056566670696,
0.0408272850023869));
#23309=CARTESIAN_POINT('Ctrl Pts',(0.0540676193498672,0.121610671661662,
0.0434139436387195));
#23310=CARTESIAN_POINT('Ctrl Pts',(0.0133639835211523,0.125930636937597,
0.0460006022750522));
#23311=CARTESIAN_POINT('Ctrl Pts',(-0.0273396523075625,0.130250602213533,
0.0485872609113848));
#23312=CARTESIAN_POINT('Ctrl Pts',(-0.0703329267419868,0.112985517770812,
0.0511739195477175));
#23313=CARTESIAN_POINT('Ctrl Pts',(-0.0967449447385466,0.0817152626609385,
0.0537605781840501));
#23314=CARTESIAN_POINT('Ctrl Pts',(-0.115741878896724,0.0592240248649833,
0.0556210412433473));
#23315=CARTESIAN_POINT('Ctrl Pts',(-0.126160906676814,0.0294875554882879,
0.0574815043026445));
#23316=CARTESIAN_POINT('Ctrl Pts',(-0.126396145829628,-9.95859796292312E-5,
0.0593419673619417));
#23317=CARTESIAN_POINT('Origin',(0.,0.,0.12));
#23318=CARTESIAN_POINT('',(-0.126529791093031,9.025049583615E-5,0.109341967361942));
#23319=CARTESIAN_POINT('',(-0.126349242904067,8.85860673823967E-5,0.0956580326380584));
#23320=CARTESIAN_POINT('',(-0.12645,1.54856587752183E-17,0.12));
#23321=CARTESIAN_POINT('Ctrl Pts',(-0.126349242904067,8.85860673823967E-5,
0.0956580326380584));
#23322=CARTESIAN_POINT('Ctrl Pts',(-0.126441591528965,0.0135570965972842,
0.0948119253946973));
#23323=CARTESIAN_POINT('Ctrl Pts',(-0.124448136217638,0.0269990101701626,
0.0939658181513361));
#23324=CARTESIAN_POINT('Ctrl Pts',(-0.120249444863787,0.0397126388809939,
0.093119710907975));
#23325=CARTESIAN_POINT('Ctrl Pts',(-0.107413505522824,0.0785798365820317,
0.0905330522716423));
#23326=CARTESIAN_POINT('Ctrl Pts',(-0.0739673525896496,0.110640458354997,
0.0879463936353097));
#23327=CARTESIAN_POINT('Ctrl Pts',(-0.0345920580258737,0.121821308595361,
0.085359734998977));
#23328=CARTESIAN_POINT('Ctrl Pts',(0.00478323653790218,0.133002158835724,
0.0827730763626444));
#23329=CARTESIAN_POINT('Ctrl Pts',(0.0500876727322792,0.123303237543486,
0.0801864177263117));
#23330=CARTESIAN_POINT('Ctrl Pts',(0.0814342209129887,0.0969820390626645,
0.077599759089979));
#23331=CARTESIAN_POINT('Ctrl Pts',(0.112780769093698,0.0706608405818426,
0.0750131004536464));
#23332=CARTESIAN_POINT('Ctrl Pts',(0.13016942926074,0.0277173649124373,
0.0724264418173139));
#23333=CARTESIAN_POINT('Ctrl Pts',(0.12596827751407,-0.0129984006283456,
0.0698397831809812));
#23334=CARTESIAN_POINT('Ctrl Pts',(0.121767125767399,-0.0537141661691284,
0.0672531245446486));
#23335=CARTESIAN_POINT('Ctrl Pts',(0.0959761621070158,-0.0922022215812886,
0.0646664659083159));
#23336=CARTESIAN_POINT('Ctrl Pts',(0.059914723710966,-0.111567668284471,
0.0620798072719833));
#23337=CARTESIAN_POINT('Ctrl Pts',(0.0238532853149157,-0.130933114987654,
0.0594931486356506));
#23338=CARTESIAN_POINT('Ctrl Pts',(-0.0224786278168013,-0.131175952981858,
0.056906489999318));
#23339=CARTESIAN_POINT('Ctrl Pts',(-0.0587401909579078,-0.112190380850839,
0.0543198313629853));
#23340=CARTESIAN_POINT('Ctrl Pts',(-0.0950017540990138,-0.0932048087198191,
0.0517331727266527));
#23341=CARTESIAN_POINT('Ctrl Pts',(-0.12119296724951,-0.0549908264635757,
0.0491465140903201));
#23342=CARTESIAN_POINT('Ctrl Pts',(-0.125823286774378,-0.0143210998620416,
0.0465598554539874));
#23343=CARTESIAN_POINT('Ctrl Pts',(-0.126361397696569,-0.0095946821776348,
0.0462592478486778));
#23344=CARTESIAN_POINT('Ctrl Pts',(-0.12660831057823,-0.00483509759607578,
0.0459586402433681));
#23345=CARTESIAN_POINT('Ctrl Pts',(-0.126575671592806,-7.20628672610732E-5,
0.0456580326380584));
#23346=CARTESIAN_POINT('Ctrl Pts',(-0.126396145829628,-9.95859796292312E-5,
0.0593419673619417));
#23347=CARTESIAN_POINT('Ctrl Pts',(-0.12648796685852,-0.0116483513064931,
0.0600681629389771));
#23348=CARTESIAN_POINT('Ctrl Pts',(-0.125028206814926,-0.0231743653405588,
0.0607943585160125));
#23349=CARTESIAN_POINT('Ctrl Pts',(-0.121921363946098,-0.034237873926493,
0.0615205540930479));
#23350=CARTESIAN_POINT('Ctrl Pts',(-0.110855003598394,-0.0736453296270277,
0.0641072127293806));
#23351=CARTESIAN_POINT('Ctrl Pts',(-0.0788915213442898,-0.107184815251071,
0.0666938713657133));
#23352=CARTESIAN_POINT('Ctrl Pts',(-0.0400617348236378,-0.120133683626334,
0.069280530002046));
#23353=CARTESIAN_POINT('Ctrl Pts',(-0.00123194830298627,-0.133082552001597,
0.0718671886383786));
#23354=CARTESIAN_POINT('Ctrl Pts',(0.0444641424842127,-0.125440803128081,
0.0744538472747112));
#23355=CARTESIAN_POINT('Ctrl Pts',(0.0769682295152699,-0.100563001286921,
0.0770405059110438));
#23356=CARTESIAN_POINT('Ctrl Pts',(0.109472316546327,-0.0756851994457607,
0.0796271645473764));
#23357=CARTESIAN_POINT('Ctrl Pts',(0.128784399821243,-0.0335713446369571,
0.0822138231837091));
#23358=CARTESIAN_POINT('Ctrl Pts',(0.126427276285523,0.00729262199647547,
0.0848004818200417));
#23359=CARTESIAN_POINT('Ctrl Pts',(0.124070152749803,0.0481565886299079,
0.0873871404563744));
#23360=CARTESIAN_POINT('Ctrl Pts',(0.100043822403448,0.0877706670879697,
0.0899737990927071));
#23361=CARTESIAN_POINT('Ctrl Pts',(0.0648947831756147,0.108746049780439,
0.0925604577290397));
#23362=CARTESIAN_POINT('Ctrl Pts',(0.0297457439477817,0.129721432472907,
0.0951471163653723));
#23363=CARTESIAN_POINT('Ctrl Pts',(-0.0165260041615291,0.132058119399784,
0.0977337750017049));
#23364=CARTESIAN_POINT('Ctrl Pts',(-0.0536093211433369,0.114730442741844,
0.100320433638038));
#23365=CARTESIAN_POINT('Ctrl Pts',(-0.0906926381251451,0.0974027660839045,
0.10290709227437));
#23366=CARTESIAN_POINT('Ctrl Pts',(-0.11858752397945,0.0604107258411485,
0.105493750910703));
#23367=CARTESIAN_POINT('Ctrl Pts',(-0.12504939731921,0.0199921027543164,
0.108080409547035));
#23368=CARTESIAN_POINT('Ctrl Pts',(-0.126099919499473,0.0134211506765118,
0.108500928818671));
#23369=CARTESIAN_POINT('Ctrl Pts',(-0.126583971845017,0.00675963476331471,
0.108921448090306));
#23370=CARTESIAN_POINT('Ctrl Pts',(-0.126529791093031,9.025049583615E-5,
0.109341967361942));
#23371=CARTESIAN_POINT('Origin',(0.,0.,0.12));
#23372=CARTESIAN_POINT('',(-0.126296536029262,-6.10717992316628E-5,0.159341967361942));
#23373=CARTESIAN_POINT('',(-0.126453631260982,-0.000102348163238207,0.145658032638058));
#23374=CARTESIAN_POINT('',(-0.12645,1.54856587752183E-17,0.12));
#23375=CARTESIAN_POINT('Ctrl Pts',(-0.126453631260982,-0.000102348163238207,
0.145658032638058));
#23376=CARTESIAN_POINT('Ctrl Pts',(-0.126183364177612,0.031552920325249,
0.143665210546026));
#23377=CARTESIAN_POINT('Ctrl Pts',(-0.114073771100105,0.0633928690595716,
0.141672388453994));
#23378=CARTESIAN_POINT('Ctrl Pts',(-0.0925489356314354,0.0864391430514358,
0.139679566361962));
#23379=CARTESIAN_POINT('Ctrl Pts',(-0.0646099631645552,0.116352924063146,
0.13709290772563));
#23380=CARTESIAN_POINT('Ctrl Pts',(-0.0208084524006029,0.131451366650306,
0.134506249089297));
#23381=CARTESIAN_POINT('Ctrl Pts',(0.0196287675426836,0.125106932552633,
0.131919590452964));
#23382=CARTESIAN_POINT('Ctrl Pts',(0.0600659874859703,0.11876249845496,
0.129332931816632));
#23383=CARTESIAN_POINT('Ctrl Pts',(0.097138916608591,0.0909751876724545,
0.126746273180299));
#23384=CARTESIAN_POINT('Ctrl Pts',(0.114574233156503,0.0539423598350403,
0.124159614543967));
#23385=CARTESIAN_POINT('Ctrl Pts',(0.132009549704415,0.0169095319976262,
0.121572955907634));
#23386=CARTESIAN_POINT('Ctrl Pts',(0.129807253677619,-0.0293688128946969,
0.118986297271301));
#23387=CARTESIAN_POINT('Ctrl Pts',(0.108934072954415,-0.0645786240759305,
0.116399638634969));
#23388=CARTESIAN_POINT('Ctrl Pts',(0.0880608922312115,-0.099788435257164,
0.113812979998636));
#23389=CARTESIAN_POINT('Ctrl Pts',(0.0485168268116012,-0.123929712727308,
0.111226321362303));
#23390=CARTESIAN_POINT('Ctrl Pts',(0.00765986125275547,-0.126405537442516,
0.108639662725971));
#23391=CARTESIAN_POINT('Ctrl Pts',(-0.0331971043060904,-0.128881362157723,
0.106053004089638));
#23392=CARTESIAN_POINT('Ctrl Pts',(-0.0753669700041717,-0.109691734117994,
0.103466345453305));
#23393=CARTESIAN_POINT('Ctrl Pts',(-0.100339039978837,-0.0772600332835736,
0.100879686816973));
#23394=CARTESIAN_POINT('Ctrl Pts',(-0.117142637704978,-0.0554368822612891,
0.0991391354240014));
#23395=CARTESIAN_POINT('Ctrl Pts',(-0.126159269908366,-0.0276178718881664,
0.0973985840310299));
#23396=CARTESIAN_POINT('Ctrl Pts',(-0.126349242904067,8.85860673823967E-5,
0.0956580326380584));
#23397=CARTESIAN_POINT('Ctrl Pts',(-0.126529791093031,9.025049583615E-5,
0.109341967361942));
#23398=CARTESIAN_POINT('Ctrl Pts',(-0.126250700293628,-0.0342644551610371,
0.111508106726639));
#23399=CARTESIAN_POINT('Ctrl Pts',(-0.111690189779818,-0.0688279388928191,
0.113674246091336));
#23400=CARTESIAN_POINT('Ctrl Pts',(-0.0867076257192948,-0.092297473337895,
0.115840385456033));
#23401=CARTESIAN_POINT('Ctrl Pts',(-0.0568751199544048,-0.120323220412367,
0.118427044092366));
#23402=CARTESIAN_POINT('Ctrl Pts',(-0.0121812475994092,-0.132529508630403,
0.121013702728699));
#23403=CARTESIAN_POINT('Ctrl Pts',(0.0277554439013372,-0.123558363290506,
0.123600361365031));
#23404=CARTESIAN_POINT('Ctrl Pts',(0.0676921354020838,-0.114587217950609,
0.126187020001364));
#23405=CARTESIAN_POINT('Ctrl Pts',(0.102871646048582,-0.0844386390527785,
0.128773678637697));
#23406=CARTESIAN_POINT('Ctrl Pts',(0.117851793294146,-0.0463464242807743,
0.131360337274029));
#23407=CARTESIAN_POINT('Ctrl Pts',(0.13283194053971,-0.00825420950877041,
0.133946995910362));
#23408=CARTESIAN_POINT('Ctrl Pts',(0.127612724384341,0.0377816411374068,
0.136533654546694));
#23409=CARTESIAN_POINT('Ctrl Pts',(0.104485135941302,0.0715534408109559,
0.139120313183027));
#23410=CARTESIAN_POINT('Ctrl Pts',(0.0813575474982633,0.105325240484505,
0.14170697181936));
#23411=CARTESIAN_POINT('Ctrl Pts',(0.0403215867675544,0.126832989185426,
0.144293630455692));
#23412=CARTESIAN_POINT('Ctrl Pts',(-0.000609841963000384,0.126635909896556,
0.146880289092025));
#23413=CARTESIAN_POINT('Ctrl Pts',(-0.0415412706935549,0.126438830607686,
0.149466947728358));
#23414=CARTESIAN_POINT('Ctrl Pts',(-0.0823681674239554,0.104536923329025,
0.15205360636469));
#23415=CARTESIAN_POINT('Ctrl Pts',(-0.10516942503222,0.0705438627883669,
0.154640265001023));
#23416=CARTESIAN_POINT('Ctrl Pts',(-0.118984510025511,0.0499477610899654,
0.156207499121329));
#23417=CARTESIAN_POINT('Ctrl Pts',(-0.126182304652747,0.0249129445447297,
0.157774733241635));
#23418=CARTESIAN_POINT('Ctrl Pts',(-0.126296536029262,-6.10717992316628E-5,
0.159341967361942));
#23419=CARTESIAN_POINT('Origin',(0.,0.,0.12));
#23420=CARTESIAN_POINT('',(-0.126625441102054,2.7778768752873E-5,0.209341967361942));
#23421=CARTESIAN_POINT('',(-0.126471935391749,0.000101176582396995,0.195658032638058));
#23422=CARTESIAN_POINT('',(-0.12645,1.54856587752183E-17,0.12));
#23423=CARTESIAN_POINT('',(0.0958116152722397,0.0825211298936481,0.24));
#23424=CARTESIAN_POINT('Ctrl Pts',(-0.126625441102054,2.7778768752873E-5,
0.209341967361942));
#23425=CARTESIAN_POINT('Ctrl Pts',(-0.126482885932031,-0.0388928622545336,
0.21180133566563));
#23426=CARTESIAN_POINT('Ctrl Pts',(-0.107125339127294,-0.077921419747323,
0.214260703969318));
#23427=CARTESIAN_POINT('Ctrl Pts',(-0.0759952538809665,-0.101287130411732,
0.216720072273006));
#23428=CARTESIAN_POINT('Ctrl Pts',(-0.0432539585932993,-0.12586218783339,
0.219306730909339));
#23429=CARTESIAN_POINT('Ctrl Pts',(0.0025100419330305,-0.133111106253138,
0.221893389545672));
#23430=CARTESIAN_POINT('Ctrl Pts',(0.0412155518054008,-0.119764891216682,
0.224480048182004));
#23431=CARTESIAN_POINT('Ctrl Pts',(0.0799210616777711,-0.106418676180227,
0.227066706818337));
#23432=CARTESIAN_POINT('Ctrl Pts',(0.111568080896182,-0.072477327687567,
0.229653365454669));
#23433=CARTESIAN_POINT('Ctrl Pts',(0.122246574267713,-0.0330282462555153,
0.232240024091002));
#23434=CARTESIAN_POINT('Ctrl Pts',(0.132925067639245,0.00642083517653631,
0.234826682727335));
#23435=CARTESIAN_POINT('Ctrl Pts',(0.122635035163896,0.0513776495479799,
0.237413341363667));
#23436=CARTESIAN_POINT('Ctrl Pts',(0.0958116152722397,0.0825211298936481,
0.24));
#23437=CARTESIAN_POINT('',(-0.0959791030802601,0.0826138105732953,0.24));
#23438=CARTESIAN_POINT('Origin',(0.,0.,0.24));
#23439=CARTESIAN_POINT('Ctrl Pts',(-0.0959791030802601,0.0826138105732953,
0.24));
#23440=CARTESIAN_POINT('Ctrl Pts',(-0.0710417758635208,0.111296717646776,
0.237599759089979));
#23441=CARTESIAN_POINT('Ctrl Pts',(-0.0322351762885183,0.128218895525122,
0.235199518179958));
#23442=CARTESIAN_POINT('Ctrl Pts',(0.00571352152256588,0.126497857083363,
0.232799277269937));
#23443=CARTESIAN_POINT('Ctrl Pts',(0.0466095526337785,0.124643152028446,
0.230212618633605));
#23444=CARTESIAN_POINT('Ctrl Pts',(0.0865092470399708,0.101136876245298,
0.227625959997272));
#23445=CARTESIAN_POINT('Ctrl Pts',(0.107920636628548,0.0662586835305903,
0.225039301360939));
#23446=CARTESIAN_POINT('Ctrl Pts',(0.129332026217125,0.0313804908158828,
0.222452642724607));
#23447=CARTESIAN_POINT('Ctrl Pts',(0.132255110988087,-0.014869618830384,
0.219865984088274));
#23448=CARTESIAN_POINT('Ctrl Pts',(0.115395215428634,-0.0521699181865619,
0.217279325451942));
#23449=CARTESIAN_POINT('Ctrl Pts',(0.0985353198691812,-0.0894702175427398,
0.214692666815609));
#23450=CARTESIAN_POINT('Ctrl Pts',(0.0618924439793129,-0.117820706608829,
0.212106008179276));
#23451=CARTESIAN_POINT('Ctrl Pts',(0.0215571925812854,-0.12478734248304,
0.209519349542944));
#23452=CARTESIAN_POINT('Ctrl Pts',(-0.0187780588167422,-0.13175397835725,
0.206932690906611));
#23453=CARTESIAN_POINT('Ctrl Pts',(-0.0628056857229291,-0.117336761039583,
0.204346032270278));
#23454=CARTESIAN_POINT('Ctrl Pts',(-0.0912027768750998,-0.0878586653637446,
0.201759373633946));
#23455=CARTESIAN_POINT('Ctrl Pts',(-0.113530209130371,-0.0646812849521466,
0.199725593301983));
#23456=CARTESIAN_POINT('Ctrl Pts',(-0.126194825294183,-0.0321932513395888,
0.197691812970021));
#23457=CARTESIAN_POINT('Ctrl Pts',(-0.126471935391749,0.000101176582396995,
0.195658032638058));
#23458=CARTESIAN_POINT('Origin',(0.,0.,0.350421172358873));
#23459=CARTESIAN_POINT('',(-0.154453350152392,-8.79343647196378E-5,0.0295788276411275));
#23460=CARTESIAN_POINT('',(-0.15422847552802,0.000108763211052777,0.025421172358873));
#23461=CARTESIAN_POINT('',(-0.1543,-1.01731279388251E-15,0.350421172358873));
#23462=CARTESIAN_POINT('',(0.15408394018464,-0.00816268198427004,0.));
#23463=CARTESIAN_POINT('Ctrl Pts',(-0.15422847552802,0.000108763211052763,
0.025421172358873));
#23464=CARTESIAN_POINT('Ctrl Pts',(-0.154338737393477,0.0139570514561378,
0.0247074241482466));
#23465=CARTESIAN_POINT('Ctrl Pts',(-0.146387882101843,0.0778735560251454,
0.0214070173012875));
#23466=CARTESIAN_POINT('Ctrl Pts',(-0.0581466660421577,0.171532975008042,
0.0155199518179959));
#23467=CARTESIAN_POINT('Ctrl Pts',(0.109502662757235,0.144085240745689,
0.00775997590899784));
#23468=CARTESIAN_POINT('Ctrl Pts',(0.156737212705124,0.0419221657566679,
0.00258665863633264));
#23469=CARTESIAN_POINT('Ctrl Pts',(0.15408394018464,-0.00816268198427004,
0.));
#23470=CARTESIAN_POINT('',(0.129620323775263,-0.0841289546921688,3.62607491890453E-17));
#23471=CARTESIAN_POINT('Origin',(0.,0.,0.));
#23472=CARTESIAN_POINT('Ctrl Pts',(-0.154453350152392,-8.7934364719636E-5,
0.0295788276411275));
#23473=CARTESIAN_POINT('Ctrl Pts',(-0.154150470777978,0.0441115087317509,
0.0272927766101045));
#23474=CARTESIAN_POINT('Ctrl Pts',(-0.111454882743928,0.138841433785012,
0.0224200669427489));
#23475=CARTESIAN_POINT('Ctrl Pts',(0.0476444145610997,0.174632482457551,
0.0149606986390605));
#23476=CARTESIAN_POINT('Ctrl Pts',(0.168251138196633,0.0613688951001999,
0.0073871404563744));
#23477=CARTESIAN_POINT('Ctrl Pts',(0.154676764047789,-0.0451013867871701,
0.00240024091002087));
#23478=CARTESIAN_POINT('Ctrl Pts',(0.129620323775263,-0.0841289546921688,
1.57209315010398E-17));
#23479=CARTESIAN_POINT('Origin',(0.,0.,0.350421172358873));
#23480=CARTESIAN_POINT('',(-0.154177051641736,0.000108096719625833,0.0795788276411275));
#23481=CARTESIAN_POINT('',(-0.154234284709463,-0.000121519309271207,0.075421172358873));
#23482=CARTESIAN_POINT('',(-0.1543,-1.01731279388251E-15,0.350421172358873));
#23483=CARTESIAN_POINT('Ctrl Pts',(-0.154234284709463,-0.000121519309271208,
0.0754211723588731));
#23484=CARTESIAN_POINT('Ctrl Pts',(-0.153947235272697,0.0359820467524117,
0.0735607092995758));
#23485=CARTESIAN_POINT('Ctrl Pts',(-0.123557126730793,0.122717061869437,
0.0691135876039459));
#23486=CARTESIAN_POINT('Ctrl Pts',(0.0191012565771036,0.180005302104073,
0.0620798072719832));
#23487=CARTESIAN_POINT('Ctrl Pts',(0.159724738700703,0.0851738948996701,
0.0543198313629854));
#23488=CARTESIAN_POINT('Ctrl Pts',(0.160113920417758,-0.0844204212478698,
0.0465598554539874));
#23489=CARTESIAN_POINT('Ctrl Pts',(0.0199582426985643,-0.179924098035372,
0.0387998795449896));
#23490=CARTESIAN_POINT('Ctrl Pts',(-0.123251388539896,-0.123176028715441,
0.0317536518466181));
#23491=CARTESIAN_POINT('Ctrl Pts',(-0.153939142967466,-0.0362298265692857,
0.0272940827845792));
#23492=CARTESIAN_POINT('Ctrl Pts',(-0.15422847552802,0.000108763211052763,
0.025421172358873));
#23493=CARTESIAN_POINT('Ctrl Pts',(-0.154177051641736,0.000108096719625859,
0.0795788276411275));
#23494=CARTESIAN_POINT('Ctrl Pts',(-0.154289739603949,0.0165429814548096,
0.0787327203977663));
#23495=CARTESIAN_POINT('Ctrl Pts',(-0.144420757340354,0.0830897487115299,
0.0752999545180725));
#23496=CARTESIAN_POINT('Ctrl Pts',(-0.0494457976037486,0.174130301808973,
0.0692805300020459));
#23497=CARTESIAN_POINT('Ctrl Pts',(0.11640175885633,0.13862511662766,0.061520554093048));
#23498=CARTESIAN_POINT('Ctrl Pts',(0.18005704388064,-0.0185795878987759,
0.0537605781840501));
#23499=CARTESIAN_POINT('Ctrl Pts',(0.0856431484406112,-0.159474177462153,
0.0460006022750521));
#23500=CARTESIAN_POINT('Ctrl Pts',(-0.0839657292871194,-0.160363143120653,
0.0382406263660544));
#23501=CARTESIAN_POINT('Ctrl Pts',(-0.151599316432495,-0.0616831513139142,
0.0327667014880793));
#23502=CARTESIAN_POINT('Ctrl Pts',(-0.154493177716258,-0.00590000442131094,
0.0298794352464371));
#23503=CARTESIAN_POINT('Ctrl Pts',(-0.154453350152392,-8.7934364719636E-5,
0.0295788276411275));
#23504=CARTESIAN_POINT('Origin',(0.,0.,0.350421172358873));
#23505=CARTESIAN_POINT('',(-0.154304431028624,-0.000124889850439479,0.129578827641127));
#23506=CARTESIAN_POINT('',(-0.154397364694779,0.000110127730384366,0.125421172358873));
#23507=CARTESIAN_POINT('',(-0.1543,-1.01731279388251E-15,0.350421172358873));
#23508=CARTESIAN_POINT('Ctrl Pts',(-0.154397364694779,0.000110127730384357,
0.125421172358873));
#23509=CARTESIAN_POINT('Ctrl Pts',(-0.154463478494948,0.00824841157753406,
0.125000653087238));
#23510=CARTESIAN_POINT('Ctrl Pts',(-0.150239588102603,0.0663774823757793,
0.121993475179269));
#23511=CARTESIAN_POINT('Ctrl Pts',(-0.0766286530280003,0.163994611436961,
0.116399638634969));
#23512=CARTESIAN_POINT('Ctrl Pts',(0.0927599764682439,0.155440618724813,
0.108639662725971));
#23513=CARTESIAN_POINT('Ctrl Pts',(0.180714016146597,0.0104239566588842,
0.100879686816973));
#23514=CARTESIAN_POINT('Ctrl Pts',(0.11001758793024,-0.143743725357685,
0.093119710907975));
#23515=CARTESIAN_POINT('Ctrl Pts',(-0.0572637123892103,-0.171718146500831,
0.0853597349989769));
#23516=CARTESIAN_POINT('Ctrl Pts',(-0.146220320052713,-0.0783754111826042,
0.0794602221492764));
#23517=CARTESIAN_POINT('Ctrl Pts',(-0.154346328875204,-0.0142138442593302,
0.0761473679359084));
#23518=CARTESIAN_POINT('Ctrl Pts',(-0.154234284709463,-0.000121519309271208,
0.0754211723588731));
#23519=CARTESIAN_POINT('Ctrl Pts',(-0.154304431028624,-0.000124889850439474,
0.129578827641127));
#23520=CARTESIAN_POINT('Ctrl Pts',(-0.153974638929265,0.0385022981904757,
0.127586005549095));
#23521=CARTESIAN_POINT('Ctrl Pts',(-0.120018027207353,0.127784966030512,
0.123006524820731));
#23522=CARTESIAN_POINT('Ctrl Pts',(0.0280571680938306,0.178826694862324,
0.115840385456033));
#23523=CARTESIAN_POINT('Ctrl Pts',(0.163771354656592,0.0771047007047774,
0.108080409547035));
#23524=CARTESIAN_POINT('Ctrl Pts',(0.155709331479018,-0.0923080778690166,
0.100320433638038));
#23525=CARTESIAN_POINT('Ctrl Pts',(0.0109489686262093,-0.180682908560435,
0.0925604577290397));
#23526=CARTESIAN_POINT('Ctrl Pts',(-0.126591758993125,-0.118094248159534,
0.0856465890634029));
#23527=CARTESIAN_POINT('Ctrl Pts',(-0.153945238013925,-0.0337005743957639,
0.0813193790340989));
#23528=CARTESIAN_POINT('Ctrl Pts',(-0.154177051641736,0.000108096719625859,
0.0795788276411275));
#23529=CARTESIAN_POINT('Origin',(0.,0.,0.350421172358873));
#23530=CARTESIAN_POINT('',(-0.154326766555531,0.000123460234585843,0.179578827641127));
#23531=CARTESIAN_POINT('',(-0.154112736333057,-7.45225671948511E-5,0.175421172358873));
#23532=CARTESIAN_POINT('',(-0.1543,-1.01731279388251E-15,0.350421172358873));
#23533=CARTESIAN_POINT('Ctrl Pts',(-0.154112736333057,-7.45225671948471E-5,
0.175421172358873));
#23534=CARTESIAN_POINT('Ctrl Pts',(-0.153973346049181,0.0303998999070902,
0.173853938238567));
#23535=CARTESIAN_POINT('Ctrl Pts',(-0.130694151755309,0.111367805862998,
0.169700045481928));
#23536=CARTESIAN_POINT('Ctrl Pts',(-0.000871711368246156,0.181012066871201,
0.162959494088956));
#23537=CARTESIAN_POINT('Ctrl Pts',(0.149350085565286,0.102277888352765,
0.155199518179958));
#23538=CARTESIAN_POINT('Ctrl Pts',(0.168456255263351,-0.0662471829332422,
0.14743954227096));
#23539=CARTESIAN_POINT('Ctrl Pts',(0.0396733728729688,-0.17661315503135,
0.139679566361963));
#23540=CARTESIAN_POINT('Ctrl Pts',(-0.115072782317819,-0.134350623919955,
0.1323401097246));
#23541=CARTESIAN_POINT('Ctrl Pts',(-0.154056805498669,-0.041811035439686,
0.12758731172357));
#23542=CARTESIAN_POINT('Ctrl Pts',(-0.154397364694779,0.000110127730384357,
0.125421172358873));
#23543=CARTESIAN_POINT('Ctrl Pts',(-0.154326766555531,0.000123460234585825,
0.179578827641127));
#23544=CARTESIAN_POINT('Ctrl Pts',(-0.154418689716183,0.0108361910665024,
0.179025949336757));
#23545=CARTESIAN_POINT('Ctrl Pts',(-0.148597337680631,0.071569631208062,
0.175886412396054));
#23546=CARTESIAN_POINT('Ctrl Pts',(-0.0683530255288039,0.167611467503216,
0.170160216819019));
#23547=CARTESIAN_POINT('Ctrl Pts',(0.100397202365132,0.150621028353064,
0.162400240910021));
#23548=CARTESIAN_POINT('Ctrl Pts',(0.18100910679194,0.00139719974911195,
0.154640265001023));
#23549=CARTESIAN_POINT('Ctrl Pts',(0.102711092909207,-0.149052183789333,
0.146880289092025));
#23550=CARTESIAN_POINT('Ctrl Pts',(-0.0657574679958034,-0.168648048308422,
0.139120313183027));
#23551=CARTESIAN_POINT('Ctrl Pts',(-0.148058381688037,-0.0731761882111772,
0.133353159366061));
#23552=CARTESIAN_POINT('Ctrl Pts',(-0.154402705029802,-0.0116353181791797,
0.130172664185428));
#23553=CARTESIAN_POINT('Ctrl Pts',(-0.154304431028624,-0.000124889850439474,
0.129578827641127));
#23554=CARTESIAN_POINT('Origin',(0.,0.,0.350421172358873));
#23555=CARTESIAN_POINT('',(-0.154128406284035,-0.000157308197905263,0.229578827641128));
#23556=CARTESIAN_POINT('',(-0.154514081154978,3.38969080117728E-5,0.225421172358873));
#23557=CARTESIAN_POINT('',(-0.1543,-1.01731279388251E-15,0.350421172358873));
#23558=CARTESIAN_POINT('',(-0.0398513841857245,-0.149064942821851,0.24));
#23559=CARTESIAN_POINT('Ctrl Pts',(-0.0398513841857245,-0.149064942821851,
0.24));
#23560=CARTESIAN_POINT('Ctrl Pts',(-0.0883048112969314,-0.136111285829332,
0.237413341363667));
#23561=CARTESIAN_POINT('Ctrl Pts',(-0.143745772087175,-0.0847488633265083,
0.233939617244043));
#23562=CARTESIAN_POINT('Ctrl Pts',(-0.154234229255939,-0.017399338864059,
0.230465893124419));
#23563=CARTESIAN_POINT('Ctrl Pts',(-0.154128406284035,-0.00015730819790527,
0.229578827641128));
#23564=CARTESIAN_POINT('',(0.0399565498027962,-0.149273502906638,0.24));
#23565=CARTESIAN_POINT('Origin',(0.,0.,0.24));
#23566=CARTESIAN_POINT('Ctrl Pts',(0.0399565498027963,-0.149273502906638,
0.24));
#23567=CARTESIAN_POINT('Ctrl Pts',(-0.00490373130458673,-0.161043406468747,
0.237599759089979));
#23568=CARTESIAN_POINT('Ctrl Pts',(-0.107666111297752,-0.141562671532916,
0.23274014987627));
#23569=CARTESIAN_POINT('Ctrl Pts',(-0.154340128899266,-0.0474588267763927,
0.227880540662561));
#23570=CARTESIAN_POINT('Ctrl Pts',(-0.154514081154978,3.3896908011755E-5,
0.225421172358873));
#23571=CARTESIAN_POINT('Origin',(0.,0.,0.350421172358873));
#23572=CARTESIAN_POINT('Ctrl Pts',(-0.154514081154978,3.3896908011755E-5,
0.225421172358873));
#23573=CARTESIAN_POINT('Ctrl Pts',(-0.154523084458981,0.00249199339844659,
0.225293882026228));
#23574=CARTESIAN_POINT('Ctrl Pts',(-0.153375868586475,0.0548933889046004,
0.222579933057251));
#23575=CARTESIAN_POINT('Ctrl Pts',(-0.0942515706791253,0.154556313135293,
0.217279325451942));
#23576=CARTESIAN_POINT('Ctrl Pts',(0.0750450248431312,0.164716481511431,
0.209519349542944));
#23577=CARTESIAN_POINT('Ctrl Pts',(0.178461260043253,0.0303012077178856,
0.201759373633945));
#23578=CARTESIAN_POINT('Ctrl Pts',(0.125203781387627,-0.130731709675357,
0.193999397724948));
#23579=CARTESIAN_POINT('Ctrl Pts',(-0.0379704533096903,-0.17698585337688,
0.18623942181595));
#23580=CARTESIAN_POINT('Ctrl Pts',(-0.141587477595567,-0.0899051669249145,
0.180046680027258));
#23581=CARTESIAN_POINT('Ctrl Pts',(-0.154203404262525,-0.019896942829432,
0.176440596874899));
#23582=CARTESIAN_POINT('Ctrl Pts',(-0.154112736333057,-7.45225671948471E-5,
0.175421172358873));
#23583=CARTESIAN_POINT('Ctrl Pts',(-0.154128406284035,-0.00015730819790527,
0.229578827641128));
#23584=CARTESIAN_POINT('Ctrl Pts',(-0.153925652370292,0.0328779499839183,
0.227879234488086));
#23585=CARTESIAN_POINT('Ctrl Pts',(-0.127638532780061,0.116591914860373,
0.223592982698713));
#23586=CARTESIAN_POINT('Ctrl Pts',(0.00818767200092134,0.180778621679153,
0.216720072273006));
#23587=CARTESIAN_POINT('Ctrl Pts',(0.154249898498561,0.0947283641859207,
0.208960096364008));
#23588=CARTESIAN_POINT('Ctrl Pts',(0.164950538597243,-0.0745810526211722,
0.201200120455011));
#23589=CARTESIAN_POINT('Ctrl Pts',(0.0308106631569891,-0.178364693496558,
0.193440144546012));
#23590=CARTESIAN_POINT('Ctrl Pts',(-0.118879635670858,-0.129347344159377,
0.186233046941385));
#23591=CARTESIAN_POINT('Ctrl Pts',(-0.153988624301243,-0.0392836590090855,
0.18161260797309));
#23592=CARTESIAN_POINT('Ctrl Pts',(-0.154326766555531,0.000123460234585825,
0.179578827641127));
#23593=CARTESIAN_POINT('Ctrl Pts',(0.0958116152722397,0.0825211298936481,
0.24));
#23594=CARTESIAN_POINT('Ctrl Pts',(0.122635035163896,0.0513776495479799,
0.237413341363667));
#23595=CARTESIAN_POINT('Ctrl Pts',(0.143215100114593,-0.0385359791949074,
0.232240024091002));
#23596=CARTESIAN_POINT('Ctrl Pts',(0.0482740424593604,-0.140360024672886,
0.224480048182004));
#23597=CARTESIAN_POINT('Ctrl Pts',(-0.0890179591196291,-0.118613269413641,
0.216720072273006));
#23598=CARTESIAN_POINT('Ctrl Pts',(-0.148173729266643,0.00709031985706173,
0.208960096364008));
#23599=CARTESIAN_POINT('Ctrl Pts',(-0.0772398646297824,0.126660050524678,
0.20120012045501));
#23600=CARTESIAN_POINT('Ctrl Pts',(0.0614999571705377,0.134986384232796,
0.193440144546013));
#23601=CARTESIAN_POINT('Ctrl Pts',(0.146250332679645,0.0248320655601208,
0.185680168637014));
#23602=CARTESIAN_POINT('Ctrl Pts',(0.102605431992647,-0.107135610424167,
0.177920192728017));
#23603=CARTESIAN_POINT('Ctrl Pts',(-0.0311170694815965,-0.145041225920327,
0.170160216819019));
#23604=CARTESIAN_POINT('Ctrl Pts',(-0.137521919612742,-0.0556176253575994,
0.162400240910021));
#23605=CARTESIAN_POINT('Ctrl Pts',(-0.123195064154356,0.0826350160503635,
0.154640265001023));
#23606=CARTESIAN_POINT('Ctrl Pts',(-0.000714373963154436,0.148340737886347,
0.146880289092025));
#23607=CARTESIAN_POINT('Ctrl Pts',(0.122393508228972,0.0838174917835845,
0.139120313183027));
#23608=CARTESIAN_POINT('Ctrl Pts',(0.138051156695079,-0.0542900601549481,
0.131360337274029));
#23609=CARTESIAN_POINT('Ctrl Pts',(0.032512624755586,-0.14473579684844,
0.123600361365031));
#23610=CARTESIAN_POINT('Ctrl Pts',(-0.101568992309399,-0.108116932194331,
0.115840385456033));
#23611=CARTESIAN_POINT('Ctrl Pts',(-0.146482409833755,0.0234186855983926,
0.108080409547036));
#23612=CARTESIAN_POINT('Ctrl Pts',(-0.0627977522708403,0.13439480632666,
0.100320433638038));
#23613=CARTESIAN_POINT('Ctrl Pts',(0.076017492057093,0.127384745546031,
0.0925604577290397));
#23614=CARTESIAN_POINT('Ctrl Pts',(0.148096483096158,0.00854251017184644,
0.0848004818200417));
#23615=CARTESIAN_POINT('Ctrl Pts',(0.0901602332714121,-0.117799054254564,
0.0770405059110438));
#23616=CARTESIAN_POINT('Ctrl Pts',(-0.0469280390901857,-0.140724300875114,
0.069280530002046));
#23617=CARTESIAN_POINT('Ctrl Pts',(-0.142818485852497,-0.0401058440029853,
0.0615205540930479));
#23618=CARTESIAN_POINT('Ctrl Pts',(-0.113326201176411,0.0957204333280909,
0.0537605781840501));
#23619=CARTESIAN_POINT('Ctrl Pts',(0.0156536221268617,0.147515686656254,
0.0460006022750521));
#23620=CARTESIAN_POINT('Ctrl Pts',(0.130895613795878,0.0698006416724775,
0.0382406263660543));
#23621=CARTESIAN_POINT('Ctrl Pts',(0.13121455111358,-0.0691831643991777,
0.0304806504570563));
#23622=CARTESIAN_POINT('Ctrl Pts',(0.0163559286405278,-0.147449139316739,
0.0227206745480584));
#23623=CARTESIAN_POINT('Ctrl Pts',(-0.112893560070904,-0.0962328986104914,
0.0149606986390606));
#23624=CARTESIAN_POINT('Ctrl Pts',(-0.142972035491037,0.0393992613429074,
0.00720072273006258));
#23625=CARTESIAN_POINT('Ctrl Pts',(-0.0476516261894416,0.140572551456688,
-0.000559253178935252));
#23626=CARTESIAN_POINT('Ctrl Pts',(0.0897382482543901,0.118078928660352,
-0.00831922908793326));
#23627=CARTESIAN_POINT('Ctrl Pts',(0.128447313976429,0.0343555272840613,
-0.0134925463605985));
#23628=CARTESIAN_POINT('Ctrl Pts',(0.126272937371016,-0.00668937872268922,
-0.0160792049969311));
#23629=CARTESIAN_POINT('Ctrl Pts',(0.102845629995666,0.0885794229410663,
0.245359734998977));
#23630=CARTESIAN_POINT('Ctrl Pts',(0.13163829265517,0.0551495423644061,
0.242773076362644));
#23631=CARTESIAN_POINT('Ctrl Pts',(0.153729244145676,-0.0413651001137901,
0.237599759089979));
#23632=CARTESIAN_POINT('Ctrl Pts',(0.0518180837997932,-0.150664563191773,
0.229839783180981));
#23633=CARTESIAN_POINT('Ctrl Pts',(-0.0955532172229155,-0.127321268762976,
0.222079807271983));
#23634=CARTESIAN_POINT('Ctrl Pts',(-0.159051911315084,0.00761085605850937,
0.214319831362985));
#23635=CARTESIAN_POINT('Ctrl Pts',(-0.0829104333128967,0.135958804728216,
0.206559855453988));
#23636=CARTESIAN_POINT('Ctrl Pts',(0.0660149797280689,0.144896416659008,
0.19879987954499));
#23637=CARTESIAN_POINT('Ctrl Pts',(0.156987308467515,0.0266551129460425,
0.191039903635992));
#23638=CARTESIAN_POINT('Ctrl Pts',(0.110138215124307,-0.11500097684123,
0.183279927726994));
#23639=CARTESIAN_POINT('Ctrl Pts',(-0.0334015307576278,-0.155689435072511,
0.175519951817996));
#23640=CARTESIAN_POINT('Ctrl Pts',(-0.147618098500879,-0.0597007962188336,
0.167759975908998));
#23641=CARTESIAN_POINT('Ctrl Pts',(-0.13223943620312,0.0887016700559064,
0.16));
#23642=CARTESIAN_POINT('Ctrl Pts',(-0.000766819764851659,0.159231180881298,
0.152240024091002));
#23643=CARTESIAN_POINT('Ctrl Pts',(0.131379034007743,0.0899709573066447,
0.144480048182004));
#23644=CARTESIAN_POINT('Ctrl Pts',(0.14818618955117,-0.0582757677477129,
0.136720072273006));
#23645=CARTESIAN_POINT('Ctrl Pts',(0.0348995407947136,-0.15536158290941,
0.128960096364009));
#23646=CARTESIAN_POINT('Ctrl Pts',(-0.109025685167754,-0.116054342400242,
0.12120012045501));
#23647=CARTESIAN_POINT('Ctrl Pts',(-0.157236423577976,0.0251379696208395,
0.113440144546013));
#23648=CARTESIAN_POINT('Ctrl Pts',(-0.0674080525232269,0.144261408030094,
0.105680168637014));
#23649=CARTESIAN_POINT('Ctrl Pts',(0.0815983201941432,0.136736703272292,
0.0979201927280168));
#23650=CARTESIAN_POINT('Ctrl Pts',(0.158968994112971,0.00916965900085902,
0.0901602168190187));
#23651=CARTESIAN_POINT('Ctrl Pts',(0.0967793514910216,-0.126447277955604,
0.0824002409100209));
#23652=CARTESIAN_POINT('Ctrl Pts',(-0.0503732635231939,-0.151055582750353,
0.0746402650010229));
#23653=CARTESIAN_POINT('Ctrl Pts',(-0.15330351242688,-0.0430502166284845,
0.066880289092025));
#23654=CARTESIAN_POINT('Ctrl Pts',(-0.121646050135849,0.102747753924341,
0.0591203131830272));
#23655=CARTESIAN_POINT('Ctrl Pts',(0.0168028336102756,0.158345558472194,
0.0513603372740292));
#23656=CARTESIAN_POINT('Ctrl Pts',(0.140505322097486,0.074925059414875,
0.0436003613650313));
#23657=CARTESIAN_POINT('Ctrl Pts',(0.140847674214973,-0.0742622500154084,
0.0358403854560334));
#23658=CARTESIAN_POINT('Ctrl Pts',(0.0175566999932067,-0.158274125556283,
0.0280804095470355));
#23659=CARTESIAN_POINT('Ctrl Pts',(-0.121181646661057,-0.103297841872129,
0.0203204336380376));
#23660=CARTESIAN_POINT('Ctrl Pts',(-0.153468334920127,0.0422917601656304,
0.0125604577290396));
#23661=CARTESIAN_POINT('Ctrl Pts',(-0.0511499728070136,0.150892692640473,
0.00480048182004178));
#23662=CARTESIAN_POINT('Ctrl Pts',(0.0963263864220051,0.126747699355464,
-0.00295949408895622));
#23663=CARTESIAN_POINT('Ctrl Pts',(0.137877280219327,0.0368777401082635,
-0.00813281136162143));
#23664=CARTESIAN_POINT('Ctrl Pts',(0.135543271642224,-0.00718047980988283,
-0.0107194699979541));
#23665=CARTESIAN_POINT('Ctrl Pts',(0.109879644719093,0.0946377159884845,
0.250719469997954));
#23666=CARTESIAN_POINT('Ctrl Pts',(0.140641550146443,0.0589214351808321,
0.248132811361621));
#23667=CARTESIAN_POINT('Ctrl Pts',(0.164243388176759,-0.0441942210326729,
0.242959494088956));
#23668=CARTESIAN_POINT('Ctrl Pts',(0.055362125140226,-0.160969101710661,
0.235199518179958));
#23669=CARTESIAN_POINT('Ctrl Pts',(-0.102088475326202,-0.13602926811231,
0.227439542270961));
#23670=CARTESIAN_POINT('Ctrl Pts',(-0.169930093363525,0.00813139225995705,
0.219679566361962));
#23671=CARTESIAN_POINT('Ctrl Pts',(-0.0885810019960112,0.145257558931755,
0.211919590452965));
#23672=CARTESIAN_POINT('Ctrl Pts',(0.0705300022856002,0.154806449085219,
0.204159614543967));
#23673=CARTESIAN_POINT('Ctrl Pts',(0.167724284255384,0.0284781603319641,
0.196399638634969));
#23674=CARTESIAN_POINT('Ctrl Pts',(0.117670998255967,-0.122866343258294,
0.188639662725971));
#23675=CARTESIAN_POINT('Ctrl Pts',(-0.0356859920336591,-0.166337644224695,
0.180879686816973));
#23676=CARTESIAN_POINT('Ctrl Pts',(-0.157714277389017,-0.0637839670800676,
0.173119710907975));
#23677=CARTESIAN_POINT('Ctrl Pts',(-0.141283808251885,0.0947683240614489,
0.165359734998977));
#23678=CARTESIAN_POINT('Ctrl Pts',(-0.000819265566548849,0.17012162387625,
0.157599759089979));
#23679=CARTESIAN_POINT('Ctrl Pts',(0.140364559786514,0.0961244228297045,
0.149839783180981));
#23680=CARTESIAN_POINT('Ctrl Pts',(0.158321222407261,-0.0622614753404775,
0.142079807271983));
#23681=CARTESIAN_POINT('Ctrl Pts',(0.0372864568338413,-0.16598736897038,
0.134319831362986));
#23682=CARTESIAN_POINT('Ctrl Pts',(-0.116482378026109,-0.123991752606152,
0.126559855453987));
#23683=CARTESIAN_POINT('Ctrl Pts',(-0.167990437322196,0.0268572536432864,
0.11879987954499));
#23684=CARTESIAN_POINT('Ctrl Pts',(-0.0720183527756138,0.154128009733527,
0.111039903635992));
#23685=CARTESIAN_POINT('Ctrl Pts',(0.0871791483311938,0.146088660998552,
0.103279927726994));
#23686=CARTESIAN_POINT('Ctrl Pts',(0.169841505129784,0.00979680782987164,
0.0955199518179957));
#23687=CARTESIAN_POINT('Ctrl Pts',(0.103398469710631,-0.135095501656644,
0.0877599759089979));
#23688=CARTESIAN_POINT('Ctrl Pts',(-0.0538184879562023,-0.161386864625592,
0.08));
#23689=CARTESIAN_POINT('Ctrl Pts',(-0.163788539001263,-0.0459945892539838,
0.0722400240910021));
#23690=CARTESIAN_POINT('Ctrl Pts',(-0.129965899095288,0.10977507452059,
0.0644800481820042));
#23691=CARTESIAN_POINT('Ctrl Pts',(0.0179520450936897,0.169175430288133,
0.0567200722730062));
#23692=CARTESIAN_POINT('Ctrl Pts',(0.150115030399095,0.0800494771572726,
0.0489600963640084));
#23693=CARTESIAN_POINT('Ctrl Pts',(0.150480797316365,-0.0793413356316391,
0.0412001204550104));
#23694=CARTESIAN_POINT('Ctrl Pts',(0.0187574713458855,-0.169099111795828,
0.0334401445460125));
#23695=CARTESIAN_POINT('Ctrl Pts',(-0.129469733251211,-0.110362785133767,
0.0256801686370146));
#23696=CARTESIAN_POINT('Ctrl Pts',(-0.163964634349217,0.0451842589883535,
0.0179201927280167));
#23697=CARTESIAN_POINT('Ctrl Pts',(-0.0546483194245858,0.161212833824257,
0.0101602168190188));
#23698=CARTESIAN_POINT('Ctrl Pts',(0.10291452458962,0.135416470050577,0.00240024091002082));
#23699=CARTESIAN_POINT('Ctrl Pts',(0.147307246462226,0.0393999529324658,
-0.00277307636264439));
#23700=CARTESIAN_POINT('Ctrl Pts',(0.144813605913432,-0.00767158089707644,
-0.00535973499897704));
#23701=CARTESIAN_POINT('Ctrl Pts',(0.116913659442519,0.100696009035903,
0.256079204996931));
#23702=CARTESIAN_POINT('Ctrl Pts',(0.149644807637716,0.0626933279972582,
0.253492546360598));
#23703=CARTESIAN_POINT('Ctrl Pts',(0.174757532207842,-0.0470233419515556,
0.248319229087933));
#23704=CARTESIAN_POINT('Ctrl Pts',(0.0589061664806588,-0.171273640229548,
0.240559253178935));
#23705=CARTESIAN_POINT('Ctrl Pts',(-0.108623733429488,-0.144737267461644,
0.232799277269938));
#23706=CARTESIAN_POINT('Ctrl Pts',(-0.180808275411966,0.00865192846140473,
0.225039301360939));
#23707=CARTESIAN_POINT('Ctrl Pts',(-0.0942515706791253,0.154556313135293,
0.217279325451942));
#23708=CARTESIAN_POINT('Ctrl Pts',(0.0750450248431312,0.164716481511431,
0.209519349542944));
#23709=CARTESIAN_POINT('Ctrl Pts',(0.178461260043253,0.0303012077178856,
0.201759373633945));
#23710=CARTESIAN_POINT('Ctrl Pts',(0.125203781387627,-0.130731709675357,
0.193999397724948));
#23711=CARTESIAN_POINT('Ctrl Pts',(-0.0379704533096903,-0.17698585337688,
0.18623942181595));
#23712=CARTESIAN_POINT('Ctrl Pts',(-0.167810456277154,-0.0678671379413016,
0.178479445906952));
#23713=CARTESIAN_POINT('Ctrl Pts',(-0.150328180300649,0.100834978066992,
0.170719469997954));
#23714=CARTESIAN_POINT('Ctrl Pts',(-0.000871711368246156,0.181012066871201,
0.162959494088956));
#23715=CARTESIAN_POINT('Ctrl Pts',(0.149350085565286,0.102277888352765,
0.155199518179958));
#23716=CARTESIAN_POINT('Ctrl Pts',(0.168456255263351,-0.0662471829332422,
0.14743954227096));
#23717=CARTESIAN_POINT('Ctrl Pts',(0.0396733728729688,-0.17661315503135,
0.139679566361963));
#23718=CARTESIAN_POINT('Ctrl Pts',(-0.123939070884463,-0.131929162812062,
0.131919590452964));
#23719=CARTESIAN_POINT('Ctrl Pts',(-0.178744451066417,0.0285765376657333,
0.124159614543967));
#23720=CARTESIAN_POINT('Ctrl Pts',(-0.0766286530280003,0.163994611436961,
0.116399638634969));
#23721=CARTESIAN_POINT('Ctrl Pts',(0.0927599764682439,0.155440618724813,
0.108639662725971));
#23722=CARTESIAN_POINT('Ctrl Pts',(0.180714016146597,0.0104239566588842,
0.100879686816973));
#23723=CARTESIAN_POINT('Ctrl Pts',(0.11001758793024,-0.143743725357685,
0.093119710907975));
#23724=CARTESIAN_POINT('Ctrl Pts',(-0.0572637123892103,-0.171718146500831,
0.0853597349989769));
#23725=CARTESIAN_POINT('Ctrl Pts',(-0.174273565575645,-0.048938961879483,
0.0775997590899791));
#23726=CARTESIAN_POINT('Ctrl Pts',(-0.138285748054726,0.11680239511684,
0.0698397831809812));
#23727=CARTESIAN_POINT('Ctrl Pts',(0.0191012565771036,0.180005302104073,
0.0620798072719832));
#23728=CARTESIAN_POINT('Ctrl Pts',(0.159724738700703,0.0851738948996701,
0.0543198313629854));
#23729=CARTESIAN_POINT('Ctrl Pts',(0.160113920417758,-0.0844204212478698,
0.0465598554539874));
#23730=CARTESIAN_POINT('Ctrl Pts',(0.0199582426985643,-0.179924098035372,
0.0387998795449896));
#23731=CARTESIAN_POINT('Ctrl Pts',(-0.137757819841364,-0.117427728395404,
0.0310399036359917));
#23732=CARTESIAN_POINT('Ctrl Pts',(-0.174460933778308,0.0480767578110765,
0.0232799277269937));
#23733=CARTESIAN_POINT('Ctrl Pts',(-0.0581466660421577,0.171532975008042,
0.0155199518179959));
#23734=CARTESIAN_POINT('Ctrl Pts',(0.109502662757235,0.144085240745689,
0.00775997590899784));
#23735=CARTESIAN_POINT('Ctrl Pts',(0.156737212705124,0.0419221657566679,
0.00258665863633264));
#23736=CARTESIAN_POINT('Ctrl Pts',(0.15408394018464,-0.00816268198427004,
0.));
#23737=CARTESIAN_POINT('Ctrl Pts',(0.15408394018464,-0.00816268198427004,
0.));
#23738=CARTESIAN_POINT('Ctrl Pts',(0.153697863146473,0.00250812953454787,
1.45220469349306E-17));
#23739=CARTESIAN_POINT('Ctrl Pts',(0.152123106309386,0.0130673133993916,
-2.32988231788825E-17));
#23740=CARTESIAN_POINT('Ctrl Pts',(0.149466152202855,0.0233620190894148,
-6.07153216591882E-17));
#23741=CARTESIAN_POINT('Ctrl Pts',(0.14793019248835,0.0293132898222067,
-8.23454409684948E-17));
#23742=CARTESIAN_POINT('Ctrl Pts',(0.146031563681721,0.0351760135160456,
3.17823908273165E-17));
#23743=CARTESIAN_POINT('Ctrl Pts',(0.143784059453749,0.0409171473780902,
6.24500451351651E-17));
#23744=CARTESIAN_POINT('Ctrl Pts',(0.142595904075608,0.0439522291322952,
7.86626679846993E-17));
#23745=CARTESIAN_POINT('Ctrl Pts',(0.141309213132582,0.0469553015723855,
1.03399090950918E-16));
#23746=CARTESIAN_POINT('Ctrl Pts',(0.13992871365498,0.0499144025840292,
1.00613961606655E-16));
#23747=CARTESIAN_POINT('Ctrl Pts',(0.135493978469587,0.0594202586791481,
9.16669744478229E-17));
#23748=CARTESIAN_POINT('Ctrl Pts',(0.130119641392827,0.0684241765595774,
5.76730757846686E-17));
#23749=CARTESIAN_POINT('Ctrl Pts',(0.123887660540245,0.0767683201192124,
1.38777878078145E-16));
#23750=CARTESIAN_POINT('Ctrl Pts',(0.120656388342022,0.0810947453345699,
1.808305895663E-16));
#23751=CARTESIAN_POINT('Ctrl Pts',(0.117193874983239,0.0852432898306738,
1.062697842984E-16));
#23752=CARTESIAN_POINT('Ctrl Pts',(0.11350808038867,0.0891875047540603,
1.14491749414469E-16));
#23753=CARTESIAN_POINT('Ctrl Pts',(0.110158526423333,0.0927719043720516,
1.21963656801269E-16));
#23754=CARTESIAN_POINT('Ctrl Pts',(0.106618991420749,0.0961915975683434,
1.17223950247179E-16));
#23755=CARTESIAN_POINT('Ctrl Pts',(0.102922970874274,0.0994011657423757,
1.02348685082632E-16));
#23756=CARTESIAN_POINT('Ctrl Pts',(0.0973787571548163,0.104215676830788,
8.00350512245867E-17));
#23757=CARTESIAN_POINT('Ctrl Pts',(0.0914754811895955,0.108568278221023,
6.56075743842472E-17));
#23758=CARTESIAN_POINT('Ctrl Pts',(0.0852365492443714,0.11239450959967,
3.29597460435593E-17));
#23759=CARTESIAN_POINT('Ctrl Pts',(0.0787787796913796,0.116354950379705,
-7.26807264206779E-19));
#23760=CARTESIAN_POINT('Ctrl Pts',(0.0719608771003193,0.11975150351845,
7.81983513604452E-17));
#23761=CARTESIAN_POINT('Ctrl Pts',(0.0648645680501024,0.122569786811788,
1.05818132034585E-16));
#23762=CARTESIAN_POINT('Ctrl Pts',(0.0619760396963809,0.123716959397427,
1.17060669392563E-16));
#23763=CARTESIAN_POINT('Ctrl Pts',(0.0590419697559043,0.124767587801255,
-1.70921410850511E-17));
#23764=CARTESIAN_POINT('Ctrl Pts',(0.0560804949635964,0.12571697313192,
-8.67361737988404E-19));
#23765=CARTESIAN_POINT('Ctrl Pts',(0.0481895916857994,0.128246627558523,
4.23638569993146E-17));
#23766=CARTESIAN_POINT('Ctrl Pts',(0.040081547172159,0.13006877931966,2.48189907303608E-17));
#23767=CARTESIAN_POINT('Ctrl Pts',(0.0318655688619291,0.131172622122806,
0.));
#23768=CARTESIAN_POINT('Ctrl Pts',(0.0267717292715239,0.131856995664207,
-1.5387571972871E-17));
#23769=CARTESIAN_POINT('Ctrl Pts',(0.0216363184326117,0.132264755542675,
5.61228976213782E-17));
#23770=CARTESIAN_POINT('Ctrl Pts',(0.0164863123329273,0.132388468809724,
3.03576608295941E-17));
#23771=CARTESIAN_POINT('Ctrl Pts',(0.0120733572364389,0.13249447666326,
8.27985532573229E-18));
#23772=CARTESIAN_POINT('Ctrl Pts',(0.00764667637530932,0.132391154756805,
7.9933444120104E-17));
#23773=CARTESIAN_POINT('Ctrl Pts',(0.00324855819595315,0.132074892239241,
9.62771529167128E-17));
#23774=CARTESIAN_POINT('Ctrl Pts',(-0.00215998367955725,0.131685971569047,
1.16375665467493E-16));
#23775=CARTESIAN_POINT('Ctrl Pts',(-0.00753310453775717,0.130975837616781,
1.12286849362194E-16));
#23776=CARTESIAN_POINT('Ctrl Pts',(-0.0128378223015392,0.129936202211006,
1.27068494615301E-16));
#23777=CARTESIAN_POINT('Ctrl Pts',(-0.0180922709275414,0.128906418710228,
1.41710064449709E-16));
#23778=CARTESIAN_POINT('Ctrl Pts',(-0.023283936630727,0.12755123862641,
1.19281234835921E-16));
#23779=CARTESIAN_POINT('Ctrl Pts',(-0.028350637156304,0.125868914531291,
9.19403442267708E-17));
#23780=CARTESIAN_POINT('Ctrl Pts',(-0.0326437071621008,0.124443463179602,
6.87741127091605E-17));
#23781=CARTESIAN_POINT('Ctrl Pts',(-0.0368509055758185,0.122782751372096,
3.08039683582783E-17));
#23782=CARTESIAN_POINT('Ctrl Pts',(-0.0409513668396969,0.120880349084932,
-1.95156391047391E-18));
#23783=CARTESIAN_POINT('Ctrl Pts',(-0.0436523616789034,0.119627226953286,
-2.45035827619675E-17));
#23784=CARTESIAN_POINT('Ctrl Pts',(-0.0463070048384274,0.118269169850402,
-4.56986185075063E-18));
#23785=CARTESIAN_POINT('Ctrl Pts',(-0.0489111879062984,0.116810626195002,
-1.73472347597681E-18));
#23786=CARTESIAN_POINT('Ctrl Pts',(0.0958116152722397,0.0825211298936481,
0.24));
#23787=CARTESIAN_POINT('Ctrl Pts',(0.102494250906434,0.0762804363331629,
0.24));
#23788=CARTESIAN_POINT('Ctrl Pts',(0.108399952301676,0.0693089192431419,
0.24));
#23789=CARTESIAN_POINT('Ctrl Pts',(0.113520383394708,0.0617855200816623,
0.24));
#23790=CARTESIAN_POINT('Ctrl Pts',(0.11760088593285,0.0557900777417299,
0.24));
#23791=CARTESIAN_POINT('Ctrl Pts',(0.1211824537664,0.0494427873910869,0.24));
#23792=CARTESIAN_POINT('Ctrl Pts',(0.124247292533427,0.0428169095598754,
0.24));
#23793=CARTESIAN_POINT('Ctrl Pts',(0.125635784531567,0.0398151273949318,
0.24));
#23794=CARTESIAN_POINT('Ctrl Pts',(0.126914357096627,0.0367636074968772,
0.24));
#23795=CARTESIAN_POINT('Ctrl Pts',(0.128080244072735,0.0336751552254939,
0.24));
#23796=CARTESIAN_POINT('Ctrl Pts',(0.13155694143068,0.024465331227027,0.24));
#23797=CARTESIAN_POINT('Ctrl Pts',(0.134041462136676,0.0149150332268467,
0.24));
#23798=CARTESIAN_POINT('Ctrl Pts',(0.135496608205084,0.00520422800883078,
0.24));
#23799=CARTESIAN_POINT('Ctrl Pts',(0.136052940597398,0.00149158663520877,
0.24));
#23800=CARTESIAN_POINT('Ctrl Pts',(0.136458356591543,-0.00224482315054724,
0.24));
#23801=CARTESIAN_POINT('Ctrl Pts',(0.136708928272429,-0.00599574054845843,
0.24));
#23802=CARTESIAN_POINT('Ctrl Pts',(0.136894600108428,-0.00877514370161729,
0.24));
#23803=CARTESIAN_POINT('Ctrl Pts',(0.136994942037659,-0.0115613689854128,
0.24));
#23804=CARTESIAN_POINT('Ctrl Pts',(0.137008733057845,-0.0143405417274864,
0.24));
#23805=CARTESIAN_POINT('Ctrl Pts',(0.137045731231951,-0.0217964308202384,
0.24));
#23806=CARTESIAN_POINT('Ctrl Pts',(0.136462408227525,-0.0292204075226799,
0.24));
#23807=CARTESIAN_POINT('Ctrl Pts',(0.135240454646173,-0.0365388974416549,
0.24));
#23808=CARTESIAN_POINT('Ctrl Pts',(0.134058793448489,-0.0436160693529878,
0.24));
#23809=CARTESIAN_POINT('Ctrl Pts',(0.132280018312676,-0.050595007513092,
0.24));
#23810=CARTESIAN_POINT('Ctrl Pts',(0.129952822193542,-0.0574290655609092,
0.24));
#23811=CARTESIAN_POINT('Ctrl Pts',(0.128850070284018,-0.0606674134165377,
0.24));
#23812=CARTESIAN_POINT('Ctrl Pts',(0.127623182384127,-0.0638741644409745,
0.24));
#23813=CARTESIAN_POINT('Ctrl Pts',(0.126284110088584,-0.067028198101918,
0.24));
#23814=CARTESIAN_POINT('Ctrl Pts',(0.122654675969015,-0.0755769205431157,
0.24));
#23815=CARTESIAN_POINT('Ctrl Pts',(0.118195290975453,-0.0837663478860722,
0.24));
#23816=CARTESIAN_POINT('Ctrl Pts',(0.113014989178579,-0.0915013065162071,
0.24));
#23817=CARTESIAN_POINT('Ctrl Pts',(0.108985931714537,-0.0975172866704144,
0.24));
#23818=CARTESIAN_POINT('Ctrl Pts',(0.104519884911976,-0.103258562704539,
0.24));
#23819=CARTESIAN_POINT('Ctrl Pts',(0.0996546828651377,-0.108675969178894,
0.24));
#23820=CARTESIAN_POINT('Ctrl Pts',(0.0972822643803542,-0.11131765910988,
0.24));
#23821=CARTESIAN_POINT('Ctrl Pts',(0.09482095240722,-0.113875293456495,
0.24));
#23822=CARTESIAN_POINT('Ctrl Pts',(0.0922773332174137,-0.116342466058553,
0.24));
#23823=CARTESIAN_POINT('Ctrl Pts',(0.0868426048671788,-0.121613857680014,
0.24));
#23824=CARTESIAN_POINT('Ctrl Pts',(0.0810310485854155,-0.126474759557936,
0.24));
#23825=CARTESIAN_POINT('Ctrl Pts',(0.0748870600798396,-0.130870957562724,
0.24));
#23826=CARTESIAN_POINT('Ctrl Pts',(0.0715378781224404,-0.133267392228159,
0.24));
#23827=CARTESIAN_POINT('Ctrl Pts',(0.0680912231566627,-0.135524142754832,
0.24));
#23828=CARTESIAN_POINT('Ctrl Pts',(0.0645638484115253,-0.13762659390894,
0.24));
#23829=CARTESIAN_POINT('Ctrl Pts',(0.0598451535113139,-0.140439117742,0.24));
#23830=CARTESIAN_POINT('Ctrl Pts',(0.0549775790306604,-0.142978967531553,
0.24));
#23831=CARTESIAN_POINT('Ctrl Pts',(0.0499773507040556,-0.145225083935062,
0.24));
#23832=CARTESIAN_POINT('Ctrl Pts',(0.0466920976074369,-0.146700828718701,
0.24));
#23833=CARTESIAN_POINT('Ctrl Pts',(0.0433495270099635,-0.148049731670784,
0.24));
#23834=CARTESIAN_POINT('Ctrl Pts',(0.039956549802796,-0.149273502906639,
0.24));
#23835=CARTESIAN_POINT('Ctrl Pts',(-0.126296536029262,-6.10717992316628E-5,
0.159341967361942));
#23836=CARTESIAN_POINT('Ctrl Pts',(-0.12637083907321,-0.0163056929409037,
0.160361391877968));
#23837=CARTESIAN_POINT('Ctrl Pts',(-0.12344809088261,-0.0325245895549842,
0.161380816393994));
#23838=CARTESIAN_POINT('Ctrl Pts',(-0.117399968681154,-0.0474794518833934,
0.162400240910021));
#23839=CARTESIAN_POINT('Ctrl Pts',(-0.102053636235694,-0.0854254922118417,
0.164986899546353));
#23840=CARTESIAN_POINT('Ctrl Pts',(-0.0665853528586453,-0.115233359066084,
0.167573558182686));
#23841=CARTESIAN_POINT('Ctrl Pts',(-0.0265641275910804,-0.123819689910512,
0.170160216819019));
#23842=CARTESIAN_POINT('Ctrl Pts',(0.0134570976764845,-0.13240602075494,
0.172746875455351));
#23843=CARTESIAN_POINT('Ctrl Pts',(0.058031264834566,-0.119770815589554,
0.175333534091684));
#23844=CARTESIAN_POINT('Ctrl Pts',(0.0875924985281064,-0.0914586003428122,
0.177920192728017));
#23845=CARTESIAN_POINT('Ctrl Pts',(0.117153732221647,-0.0631463850960709,
0.180506851364349));
#23846=CARTESIAN_POINT('Ctrl Pts',(0.131702032450646,-0.0191571597679751,
0.183093510000682));
#23847=CARTESIAN_POINT('Ctrl Pts',(0.124851119980295,0.0211965060081854,
0.185680168637015));
#23848=CARTESIAN_POINT('Ctrl Pts',(0.118000207509943,0.0615501717843459,
0.188266827273347));
#23849=CARTESIAN_POINT('Ctrl Pts',(0.0897500823402403,0.0982682780085711,
0.19085348590968));
#23850=CARTESIAN_POINT('Ctrl Pts',(0.0525017161220023,0.115239608835997,
0.193440144546013));
#23851=CARTESIAN_POINT('Ctrl Pts',(0.0152533499037644,0.132210939663423,
0.196026803182345));
#23852=CARTESIAN_POINT('Ctrl Pts',(-0.030993257363009,0.129435495094051,
0.198613461818678));
#23853=CARTESIAN_POINT('Ctrl Pts',(-0.0659388717692058,0.108119484364762,
0.20120012045501));
#23854=CARTESIAN_POINT('Ctrl Pts',(-0.100884486175403,0.0868034736354726,
0.203786779091343));
#23855=CARTESIAN_POINT('Ctrl Pts',(-0.124529107721023,0.0469468967462671,
0.206373437727676));
#23856=CARTESIAN_POINT('Ctrl Pts',(-0.126492123469331,0.00606801008988057,
0.208960096364008));
#23857=CARTESIAN_POINT('Ctrl Pts',(-0.126588724127832,0.00405634646811867,
0.209087386696653));
#23858=CARTESIAN_POINT('Ctrl Pts',(-0.126632819376787,0.00204220716288977,
0.209214677029297));
#23859=CARTESIAN_POINT('Ctrl Pts',(-0.126625441102054,2.7778768752873E-5,
0.209341967361942));
#23860=CARTESIAN_POINT('Ctrl Pts',(-0.0398513841857245,-0.149064942821851,
0.24));
#23861=CARTESIAN_POINT('Ctrl Pts',(-0.0883048112969314,-0.136111285829332,
0.237413341363667));
#23862=CARTESIAN_POINT('Ctrl Pts',(-0.170871437255804,-0.0596187094618861,
0.232240024091002));
#23863=CARTESIAN_POINT('Ctrl Pts',(-0.145169204726118,0.108307533342445,
0.224480048182004));
#23864=CARTESIAN_POINT('Ctrl Pts',(0.00818767200092134,0.180778621679153,
0.216720072273006));
#23865=CARTESIAN_POINT('Ctrl Pts',(0.154249898498561,0.0947283641859207,
0.208960096364008));
#23866=CARTESIAN_POINT('Ctrl Pts',(0.164950538597243,-0.0745810526211722,
0.201200120455011));
#23867=CARTESIAN_POINT('Ctrl Pts',(0.0308106631569891,-0.178364693496558,
0.193440144546012));
#23868=CARTESIAN_POINT('Ctrl Pts',(-0.13036283225522,-0.125587074703769,
0.185680168637015));
#23869=CARTESIAN_POINT('Ctrl Pts',(-0.17709781441264,0.03745832727601,0.177920192728017));
#23870=CARTESIAN_POINT('Ctrl Pts',(-0.0683530255288039,0.167611467503216,
0.170160216819019));
#23871=CARTESIAN_POINT('Ctrl Pts',(0.100397202365132,0.150621028353064,
0.162400240910021));
#23872=CARTESIAN_POINT('Ctrl Pts',(0.18100910679194,0.00139719974911195,
0.154640265001023));
#23873=CARTESIAN_POINT('Ctrl Pts',(0.102711092909207,-0.149052183789333,
0.146880289092025));
#23874=CARTESIAN_POINT('Ctrl Pts',(-0.0657574679958034,-0.168648048308422,
0.139120313183027));
#23875=CARTESIAN_POINT('Ctrl Pts',(-0.176497206835689,-0.0401861834345609,
0.131360337274029));
#23876=CARTESIAN_POINT('Ctrl Pts',(-0.132288575936487,0.123555290563421,
0.123600361365031));
#23877=CARTESIAN_POINT('Ctrl Pts',(0.0280571680938306,0.178826694862324,
0.115840385456033));
#23878=CARTESIAN_POINT('Ctrl Pts',(0.163771354656592,0.0771047007047774,
0.108080409547035));
#23879=CARTESIAN_POINT('Ctrl Pts',(0.155709331479018,-0.0923080778690166,
0.100320433638038));
#23880=CARTESIAN_POINT('Ctrl Pts',(0.0109489686262093,-0.180682908560435,
0.0925604577290397));
#23881=CARTESIAN_POINT('Ctrl Pts',(-0.143423754439364,-0.110434756566834,
0.0848004818200417));
#23882=CARTESIAN_POINT('Ctrl Pts',(-0.17188331593326,0.0567648465404429,
0.0770405059110439));
#23883=CARTESIAN_POINT('Ctrl Pts',(-0.0494457976037486,0.174130301808973,
0.0692805300020459));
#23884=CARTESIAN_POINT('Ctrl Pts',(0.11640175885633,0.13862511662766,0.061520554093048));
#23885=CARTESIAN_POINT('Ctrl Pts',(0.18005704388064,-0.0185795878987759,
0.0537605781840501));
#23886=CARTESIAN_POINT('Ctrl Pts',(0.0856431484406112,-0.159474177462153,
0.0460006022750521));
#23887=CARTESIAN_POINT('Ctrl Pts',(-0.0839657292871194,-0.160363143120653,
0.0382406263660544));
#23888=CARTESIAN_POINT('Ctrl Pts',(-0.179844832231877,-0.0204718628801216,
0.0304806504570563));
#23889=CARTESIAN_POINT('Ctrl Pts',(-0.117866479118068,0.137399078213474,
0.0227206745480585));
#23890=CARTESIAN_POINT('Ctrl Pts',(0.0476444145610997,0.174632482457551,
0.0149606986390605));
#23891=CARTESIAN_POINT('Ctrl Pts',(0.171219786572432,0.0585809927800803,
0.00720072273006264));
#23892=CARTESIAN_POINT('Ctrl Pts',(0.144688050375066,-0.108949473877577,
-0.000559253178935319));
#23893=CARTESIAN_POINT('Ctrl Pts',(-0.0092814439579932,-0.180735423716049,
-0.00831922908793317));
#23894=CARTESIAN_POINT('Ctrl Pts',(-0.105867686800049,-0.122947365648507,
-0.0134925463605985));
#23895=CARTESIAN_POINT('Ctrl Pts',(-0.131895903200816,-0.0800747195988904,
-0.0160792049969312));
#23896=CARTESIAN_POINT('Ctrl Pts',(-0.0374537582415196,-0.140096572423086,
0.245359734998977));
#23897=CARTESIAN_POINT('Ctrl Pts',(-0.0829920245295529,-0.127922261611689,
0.242773076362644));
#23898=CARTESIAN_POINT('Ctrl Pts',(-0.160591096949962,-0.0560317985556137,
0.237599759089979));
#23899=CARTESIAN_POINT('Ctrl Pts',(-0.13643521822445,0.101791299158848,
0.229839783180981));
#23900=CARTESIAN_POINT('Ctrl Pts',(0.00769506740980954,0.1699022237233,
0.222079807271983));
#23901=CARTESIAN_POINT('Ctrl Pts',(0.144969579481095,0.0890291096113304,
0.214319831362985));
#23902=CARTESIAN_POINT('Ctrl Pts',(0.155026424317845,-0.0700939445729984,
0.206559855453987));
#23903=CARTESIAN_POINT('Ctrl Pts',(0.0289569648011409,-0.167633527556011,
0.19879987954499));
#23904=CARTESIAN_POINT('Ctrl Pts',(-0.122519659046519,-0.118031231043151,
0.191039903635991));
#23905=CARTESIAN_POINT('Ctrl Pts',(-0.166442869216287,0.0352046776440443,
0.183279927726994));
#23906=CARTESIAN_POINT('Ctrl Pts',(-0.064240621638164,0.157527260611955,
0.175519951817996));
#23907=CARTESIAN_POINT('Ctrl Pts',(0.0943568867767351,0.141559037340679,
0.167759975908998));
#23908=CARTESIAN_POINT('Ctrl Pts',(0.170118841887737,0.00131313836865665,
0.16));
#23909=CARTESIAN_POINT('Ctrl Pts',(0.0965315639882279,-0.140084581027326,
0.152240024091002));
#23910=CARTESIAN_POINT('Ctrl Pts',(-0.0618012237018238,-0.158501476380598,
0.144480048182004));
#23911=CARTESIAN_POINT('Ctrl Pts',(-0.165878396703103,-0.0377684145673052,
0.136720072273006));
#23912=CARTESIAN_POINT('Ctrl Pts',(-0.124329541933827,0.116121687534276,
0.128960096364008));
#23913=CARTESIAN_POINT('Ctrl Pts',(0.0263691315170036,0.168067732987372,
0.12120012045501));
#23914=CARTESIAN_POINT('Ctrl Pts',(0.153918185014798,0.0724657594331675,
0.113440144546012));
#23915=CARTESIAN_POINT('Ctrl Pts',(0.146341206869619,-0.0867544378416841,
0.105680168637015));
#23916=CARTESIAN_POINT('Ctrl Pts',(0.0102902328814698,-0.169812269106107,
0.0979201927280167));
#23917=CARTESIAN_POINT('Ctrl Pts',(-0.134794781526993,-0.103790539737311,
0.0901602168190187));
#23918=CARTESIAN_POINT('Ctrl Pts',(-0.161542096774173,0.0533496359633175,
0.0824002409100209));
#23919=CARTESIAN_POINT('Ctrl Pts',(-0.0464709316213242,0.163653894581969,
0.074640265001023));
#23920=CARTESIAN_POINT('Ctrl Pts',(0.109398542213106,0.130284849835523,
0.066880289092025));
#23921=CARTESIAN_POINT('Ctrl Pts',(0.16922405906302,-0.0174617621848401,
0.0591203131830272));
#23922=CARTESIAN_POINT('Ctrl Pts',(0.0804904984426183,-0.149879543972585,
0.0513603372740291));
#23923=CARTESIAN_POINT('Ctrl Pts',(-0.0789139998409189,-0.150715025739123,
0.0436003613650314));
#23924=CARTESIAN_POINT('Ctrl Pts',(-0.169024614954586,-0.0192401899891918,
0.0358403854560333));
#23925=CARTESIAN_POINT('Ctrl Pts',(-0.110775138777956,0.12913257502003,
0.0280804095470356));
#23926=CARTESIAN_POINT('Ctrl Pts',(0.0447779273164969,0.164125861942445,
0.0203204336380375));
#23927=CARTESIAN_POINT('Ctrl Pts',(0.16091848811479,0.0550565152494576,
0.0125604577290397));
#23928=CARTESIAN_POINT('Ctrl Pts',(0.135983012131502,-0.10239461786658,
0.00480048182004171));
#23929=CARTESIAN_POINT('Ctrl Pts',(-0.00872303347143,-0.169861624730324,
-0.00295949408895612));
#23930=CARTESIAN_POINT('Ctrl Pts',(-0.0994982439886826,-0.115550337924785,
-0.00813281136162148));
#23931=CARTESIAN_POINT('Ctrl Pts',(-0.123960494032221,-0.0752570895690155,
-0.0107194699979541));
#23932=CARTESIAN_POINT('Ctrl Pts',(-0.0350561322973148,-0.13112820202432,
0.250719469997954));
#23933=CARTESIAN_POINT('Ctrl Pts',(-0.0776792377621743,-0.119733237394047,
0.248132811361621));
#23934=CARTESIAN_POINT('Ctrl Pts',(-0.150310756644121,-0.0524448876493412,
0.242959494088956));
#23935=CARTESIAN_POINT('Ctrl Pts',(-0.127701231722781,0.0952750649752511,
0.235199518179958));
#23936=CARTESIAN_POINT('Ctrl Pts',(0.00720246281869772,0.159025825767447,
0.22743954227096));
#23937=CARTESIAN_POINT('Ctrl Pts',(0.135689260463629,0.08332985503674,0.219679566361962));
#23938=CARTESIAN_POINT('Ctrl Pts',(0.145102310038447,-0.0656068365248246,
0.211919590452964));
#23939=CARTESIAN_POINT('Ctrl Pts',(0.0271032664452926,-0.156902361615465,
0.204159614543967));
#23940=CARTESIAN_POINT('Ctrl Pts',(-0.114676485837817,-0.110475387382534,
0.196399638634969));
#23941=CARTESIAN_POINT('Ctrl Pts',(-0.155787924019933,0.0329510280120788,
0.188639662725971));
#23942=CARTESIAN_POINT('Ctrl Pts',(-0.0601282177475243,0.147443053720694,
0.180879686816973));
#23943=CARTESIAN_POINT('Ctrl Pts',(0.0883165711883383,0.132497046328295,
0.173119710907975));
#23944=CARTESIAN_POINT('Ctrl Pts',(0.159228576983534,0.00122907698820117,
0.165359734998977));
#23945=CARTESIAN_POINT('Ctrl Pts',(0.0903520350672485,-0.131116978265319,
0.157599759089979));
#23946=CARTESIAN_POINT('Ctrl Pts',(-0.0578449794078444,-0.148354904452775,
0.149839783180981));
#23947=CARTESIAN_POINT('Ctrl Pts',(-0.155259586570517,-0.0353506457000499,
0.142079807271983));
#23948=CARTESIAN_POINT('Ctrl Pts',(-0.116370507931168,0.108688084505131,
0.134319831362985));
#23949=CARTESIAN_POINT('Ctrl Pts',(0.0246810949401768,0.157308771112418,
0.126559855453988));
#23950=CARTESIAN_POINT('Ctrl Pts',(0.144065015373005,0.0678268181615582,
0.118799879544989));
#23951=CARTESIAN_POINT('Ctrl Pts',(0.13697308226022,-0.0812007978143519,
0.111039903635992));
#23952=CARTESIAN_POINT('Ctrl Pts',(0.00963149713673027,-0.15894162965178,
0.103279927726994));
#23953=CARTESIAN_POINT('Ctrl Pts',(-0.126165808614623,-0.0971463229077874,
0.0955199518179957));
#23954=CARTESIAN_POINT('Ctrl Pts',(-0.151200877615086,0.0499344253861922,
0.087759975908998));
#23955=CARTESIAN_POINT('Ctrl Pts',(-0.0434960656388994,0.153177487354966,
0.08));
#23956=CARTESIAN_POINT('Ctrl Pts',(0.102395325569881,0.121944583043386,
0.072240024091002));
#23957=CARTESIAN_POINT('Ctrl Pts',(0.158391074245402,-0.0163439364709043,
0.0644800481820042));
#23958=CARTESIAN_POINT('Ctrl Pts',(0.0753378484446251,-0.140284910483017,
0.0567200722730062));
#23959=CARTESIAN_POINT('Ctrl Pts',(-0.0738622703947183,-0.141066908357593,
0.0489600963640083));
#23960=CARTESIAN_POINT('Ctrl Pts',(-0.158204397677296,-0.018008517098262,
0.0412001204550104));
#23961=CARTESIAN_POINT('Ctrl Pts',(-0.103683798437843,0.120866071826586,
0.0334401445460125));
#23962=CARTESIAN_POINT('Ctrl Pts',(0.0419114400718942,0.153619241427338,
0.0256801686370146));
#23963=CARTESIAN_POINT('Ctrl Pts',(0.150617189657149,0.051532037718835,
0.0179201927280167));
#23964=CARTESIAN_POINT('Ctrl Pts',(0.127277973887939,-0.0958397618555833,
0.0101602168190187));
#23965=CARTESIAN_POINT('Ctrl Pts',(-0.00816462298486686,-0.1589878257446,
0.00240024091002091));
#23966=CARTESIAN_POINT('Ctrl Pts',(-0.0931288011773165,-0.108153310201063,
-0.00277307636264444));
#23967=CARTESIAN_POINT('Ctrl Pts',(-0.116025084863626,-0.0704394595391406,
-0.00535973499897709));
#23968=CARTESIAN_POINT('Ctrl Pts',(-0.0326585063531099,-0.122159831625555,
0.256079204996931));
#23969=CARTESIAN_POINT('Ctrl Pts',(-0.0723664509947957,-0.111544213176404,
0.253492546360598));
#23970=CARTESIAN_POINT('Ctrl Pts',(-0.140030416338279,-0.0488579767430688,
0.248319229087933));
#23971=CARTESIAN_POINT('Ctrl Pts',(-0.118967245221113,0.0887588307916541,
0.240559253178936));
#23972=CARTESIAN_POINT('Ctrl Pts',(0.00670985822758596,0.148149427811594,
0.232799277269937));
#23973=CARTESIAN_POINT('Ctrl Pts',(0.126408941446163,0.0776306004621497,
0.225039301360939));
#23974=CARTESIAN_POINT('Ctrl Pts',(0.13517819575905,-0.0611197284766509,
0.217279325451942));
#23975=CARTESIAN_POINT('Ctrl Pts',(0.0252495680894444,-0.146171195674918,
0.209519349542944));
#23976=CARTESIAN_POINT('Ctrl Pts',(-0.106833312629116,-0.102919543721916,
0.201759373633946));
#23977=CARTESIAN_POINT('Ctrl Pts',(-0.14513297882358,0.0306973783801131,
0.193999397724948));
#23978=CARTESIAN_POINT('Ctrl Pts',(-0.0560158138568844,0.137358846829434,
0.18623942181595));
#23979=CARTESIAN_POINT('Ctrl Pts',(0.0822762555999414,0.12343505531591,
0.178479445906952));
#23980=CARTESIAN_POINT('Ctrl Pts',(0.148338312079331,0.00114501560774606,
0.170719469997954));
#23981=CARTESIAN_POINT('Ctrl Pts',(0.0841725061462688,-0.122149375503312,
0.162959494088956));
#23982=CARTESIAN_POINT('Ctrl Pts',(-0.0538887351138648,-0.138208332524951,
0.155199518179959));
#23983=CARTESIAN_POINT('Ctrl Pts',(-0.144640776437932,-0.0329328768327946,
0.14743954227096));
#23984=CARTESIAN_POINT('Ctrl Pts',(-0.108411473928508,0.101254481475986,
0.139679566361963));
#23985=CARTESIAN_POINT('Ctrl Pts',(0.0229930583633497,0.146549809237466,
0.131919590452964));
#23986=CARTESIAN_POINT('Ctrl Pts',(0.134211845731212,0.0631878768899486,
0.124159614543967));
#23987=CARTESIAN_POINT('Ctrl Pts',(0.127604957650822,-0.0756471577870196,
0.116399638634969));
#23988=CARTESIAN_POINT('Ctrl Pts',(0.00897276139199077,-0.148070990197453,
0.108639662725971));
#23989=CARTESIAN_POINT('Ctrl Pts',(-0.117536835702253,-0.0905021060782641,
0.100879686816973));
#23990=CARTESIAN_POINT('Ctrl Pts',(-0.140859658455999,0.0465192148090667,
0.0931197109079749));
#23991=CARTESIAN_POINT('Ctrl Pts',(-0.0405211996564747,0.142701080127962,
0.0853597349989771));
#23992=CARTESIAN_POINT('Ctrl Pts',(0.0953921089266558,0.113604316251249,
0.077599759089979));
#23993=CARTESIAN_POINT('Ctrl Pts',(0.147558089427783,-0.0152261107569683,
0.0698397831809813));
#23994=CARTESIAN_POINT('Ctrl Pts',(0.070185198446632,-0.130690276993449,
0.0620798072719832));
#23995=CARTESIAN_POINT('Ctrl Pts',(-0.0688105409485176,-0.131418790976063,
0.0543198313629854));
#23996=CARTESIAN_POINT('Ctrl Pts',(-0.147384180400005,-0.0167768442073323,
0.0465598554539874));
#23997=CARTESIAN_POINT('Ctrl Pts',(-0.0965924580977301,0.112599568633142,
0.0387998795449896));
#23998=CARTESIAN_POINT('Ctrl Pts',(0.0390449528272914,0.143112620912232,
0.0310399036359916));
#23999=CARTESIAN_POINT('Ctrl Pts',(0.140315891199508,0.0480075601882123,
0.0232799277269937));
#24000=CARTESIAN_POINT('Ctrl Pts',(0.118572935644375,-0.0892849058445864,
0.0155199518179958));
#24001=CARTESIAN_POINT('Ctrl Pts',(-0.00760621249830358,-0.148114026758875,
0.00775997590899793));
#24002=CARTESIAN_POINT('Ctrl Pts',(-0.0867593583659504,-0.100756282477341,
0.00258665863633259));
#24003=CARTESIAN_POINT('Ctrl Pts',(-0.108089675695031,-0.0656218295092657,
-5.55111512312578E-17));
#24004=CARTESIAN_POINT('Ctrl Pts',(-0.108089675695031,-0.0656218295092657,
-5.55111512312578E-17));
#24005=CARTESIAN_POINT('Ctrl Pts',(-0.104219465379748,-0.0739058869203245,
-4.02841154597017E-17));
#24006=CARTESIAN_POINT('Ctrl Pts',(-0.0994141168358061,-0.0816768736924768,
-5.16144647363644E-17));
#24007=CARTESIAN_POINT('Ctrl Pts',(-0.0938412360364922,-0.088871564406415,
-3.81639164714898E-17));
#24008=CARTESIAN_POINT('Ctrl Pts',(-0.0894001862863345,-0.094605040600905,
-2.74451237748006E-17));
#24009=CARTESIAN_POINT('Ctrl Pts',(-0.0844703330957707,-0.0999727304469881,
3.12377098840079E-17));
#24010=CARTESIAN_POINT('Ctrl Pts',(-0.0791158513129458,-0.104935071387697,
-1.21430643318376E-17));
#24011=CARTESIAN_POINT('Ctrl Pts',(-0.0766900604813501,-0.107183206995485,
-3.17962611543325E-17));
#24012=CARTESIAN_POINT('Ctrl Pts',(-0.0741829996358932,-0.109342173006691,
4.83248416902999E-17));
#24013=CARTESIAN_POINT('Ctrl Pts',(-0.0716059924168524,-0.111405381598006,
5.3776427755281E-17));
#24014=CARTESIAN_POINT('Ctrl Pts',(-0.0639212992135713,-0.117557915794061,
7.00331794132204E-17));
#24015=CARTESIAN_POINT('Ctrl Pts',(-0.0556061968393146,-0.12287204611112,
-5.69073736333764E-18));
#24016=CARTESIAN_POINT('Ctrl Pts',(-0.0468203466856493,-0.127256781127915,
5.55111512312578E-17));
#24017=CARTESIAN_POINT('Ctrl Pts',(-0.0434613267337519,-0.12893315986732,
7.89099528597243E-17));
#24018=CARTESIAN_POINT('Ctrl Pts',(-0.0400330653128497,-0.130473352587733,
3.97002991909352E-17));
#24019=CARTESIAN_POINT('Ctrl Pts',(-0.0365431560942257,-0.131870761756357,
6.59194920871187E-17));
#24020=CARTESIAN_POINT('Ctrl Pts',(-0.0339571636773035,-0.13290622981212,
8.5347686277821E-17));
#24021=CARTESIAN_POINT('Ctrl Pts',(-0.0313383144727484,-0.133862652235137,
-2.74403076010104E-17));
#24022=CARTESIAN_POINT('Ctrl Pts',(-0.0286994266230122,-0.134734580282325,
-2.42861286636753E-17));
#24023=CARTESIAN_POINT('Ctrl Pts',(-0.0216199050576346,-0.137073760181214,
-1.58242011095522E-17));
#24024=CARTESIAN_POINT('Ctrl Pts',(-0.0143790427459088,-0.138813119073991,
5.80198461902811E-17));
#24025=CARTESIAN_POINT('Ctrl Pts',(-0.0070411538297537,-0.139912507657099,
6.93889390390723E-17));
#24026=CARTESIAN_POINT('Ctrl Pts',(5.47883476400097E-5,-0.140975646920361,
8.02325614020808E-17));
#24027=CARTESIAN_POINT('Ctrl Pts',(0.00724182591717642,-0.141440539972256,
1.32011341321413E-16));
#24028=CARTESIAN_POINT('Ctrl Pts',(0.0144605478337719,-0.141339082434075,
1.61329283265843E-16));
#24029=CARTESIAN_POINT('Ctrl Pts',(0.0178811722145177,-0.141291006315792,
1.75221724083914E-16));
#24030=CARTESIAN_POINT('Ctrl Pts',(0.021310106848269,-0.141115105569205,
1.85534911235541E-16));
#24031=CARTESIAN_POINT('Ctrl Pts',(0.0247235715439624,-0.140816220288761,
1.71737624121704E-16));
#24032=CARTESIAN_POINT('Ctrl Pts',(0.0339754553361668,-0.140006119078294,
1.34341339582434E-16));
#24033=CARTESIAN_POINT('Ctrl Pts',(0.0431421008898472,-0.138295657968001,
8.04496487960062E-17));
#24034=CARTESIAN_POINT('Ctrl Pts',(0.0520992976556894,-0.135759125106636,
3.20923843055709E-17));
#24035=CARTESIAN_POINT('Ctrl Pts',(0.0590658916121619,-0.13378629867842,
-5.518202506064E-18));
#24036=CARTESIAN_POINT('Ctrl Pts',(0.0659062642374416,-0.131312982137409,
7.87850579480063E-17));
#24037=CARTESIAN_POINT('Ctrl Pts',(0.0725619642951071,-0.128359965266718,
7.63278329429795E-17));
#24038=CARTESIAN_POINT('Ctrl Pts',(0.0758074813473741,-0.126919986522721,
7.51296170399226E-17));
#24039=CARTESIAN_POINT('Ctrl Pts',(0.0790005264283722,-0.125369490597537,
8.38688896655138E-17));
#24040=CARTESIAN_POINT('Ctrl Pts',(0.0821329715644795,-0.123712761836801,
7.24247051220317E-17));
#24041=CARTESIAN_POINT('Ctrl Pts',(0.0888257654942848,-0.120172989003949,
4.79730178566093E-17));
#24042=CARTESIAN_POINT('Ctrl Pts',(0.0952446087626691,-0.116147988031934,
8.96774285244103E-17));
#24043=CARTESIAN_POINT('Ctrl Pts',(0.101324221742587,-0.111663228753314,
8.28330459778925E-17));
#24044=CARTESIAN_POINT('Ctrl Pts',(0.104638321741973,-0.109218510516871,
7.91020571356516E-17));
#24045=CARTESIAN_POINT('Ctrl Pts',(0.107849695272814,-0.106637925639498,
3.17151869302413E-17));
#24046=CARTESIAN_POINT('Ctrl Pts',(0.110939265073957,-0.10393289123317,
1.53956708492942E-17));
#24047=CARTESIAN_POINT('Ctrl Pts',(0.115072333360666,-0.100314234708527,
-6.43574216607592E-18));
#24048=CARTESIAN_POINT('Ctrl Pts',(0.118992075260627,-0.0964697210975667,
5.54296751400654E-17));
#24049=CARTESIAN_POINT('Ctrl Pts',(0.122673447199167,-0.0924082746861152,
3.52365706057789E-17));
#24050=CARTESIAN_POINT('Ctrl Pts',(0.125092164655522,-0.0897398425098966,
2.31620156359627E-17));
#24051=CARTESIAN_POINT('Ctrl Pts',(0.127407959881093,-0.0869777021544565,
-4.01489640485901E-17));
#24052=CARTESIAN_POINT('Ctrl Pts',(0.129620323775263,-0.0841289546921697,
-3.98986399474666E-17));
#24053=CARTESIAN_POINT('Ctrl Pts',(-0.126471935391749,0.000101176582396995,
0.195658032638058));
#24054=CARTESIAN_POINT('Ctrl Pts',(-0.126547267107008,0.00888033934128026,
0.195105154333688));
#24055=CARTESIAN_POINT('Ctrl Pts',(-0.125707148272093,0.0176451944231377,
0.194552276029318));
#24056=CARTESIAN_POINT('Ctrl Pts',(-0.12389684029672,0.0262048027713284,
0.193999397724948));
#24057=CARTESIAN_POINT('Ctrl Pts',(-0.115427257168015,0.0662512011965534,
0.191412739088615));
#24058=CARTESIAN_POINT('Ctrl Pts',(-0.0857215355124495,0.101805024012994,
0.188826080452282));
#24059=CARTESIAN_POINT('Ctrl Pts',(-0.0478199964418627,0.117261303502293,
0.18623942181595));
#24060=CARTESIAN_POINT('Ctrl Pts',(-0.0099184573712758,0.132717582991593,
0.183652763179617));
#24061=CARTESIAN_POINT('Ctrl Pts',(0.0361788991143328,0.128076319153751,
0.181066104543285));
#24062=CARTESIAN_POINT('Ctrl Pts',(0.070237920103702,0.105374013950137,
0.178479445906952));
#24063=CARTESIAN_POINT('Ctrl Pts',(0.104296941093071,0.0826717087465222,
0.175892787270619));
#24064=CARTESIAN_POINT('Ctrl Pts',(0.126317626586201,0.0419083621771342,
0.173306128634287));
#24065=CARTESIAN_POINT('Ctrl Pts',(0.126633668343922,0.000977623707263797,
0.170719469997954));
#24066=CARTESIAN_POINT('Ctrl Pts',(0.126949710101644,-0.0399531147626067,
0.168132811361621));
#24067=CARTESIAN_POINT('Ctrl Pts',(0.105561108123956,-0.08105124513296,
0.165546152725289));
#24068=CARTESIAN_POINT('Ctrl Pts',(0.0718566002584231,-0.104276803155076,
0.162959494088956));
#24069=CARTESIAN_POINT('Ctrl Pts',(0.0381520923928904,-0.127502361177192,
0.160372835452623));
#24070=CARTESIAN_POINT('Ctrl Pts',(-0.00786832136048696,-0.132855346851071,
0.157786176816291));
#24071=CARTESIAN_POINT('Ctrl Pts',(-0.0460038684578537,-0.117985930405985,
0.155199518179958));
#24072=CARTESIAN_POINT('Ctrl Pts',(-0.0841394155552204,-0.103116513960899,
0.152612859543626));
#24073=CARTESIAN_POINT('Ctrl Pts',(-0.114390095996576,-0.0680246953968468,
0.150026200907293));
#24074=CARTESIAN_POINT('Ctrl Pts',(-0.12347721913235,-0.0281142263966907,
0.14743954227096));
#24075=CARTESIAN_POINT('Ctrl Pts',(-0.125563410841138,-0.018951712774069,
0.14684570572666));
#24076=CARTESIAN_POINT('Ctrl Pts',(-0.126534167537385,-0.00953522996602069,
0.146251869182359));
#24077=CARTESIAN_POINT('Ctrl Pts',(-0.126453631260982,-0.000102348163238207,
0.145658032638058));
#24078=CARTESIAN_POINT('Ctrl Pts',(-0.0398513841857245,-0.149064942821851,
0.24));
#24079=CARTESIAN_POINT('Ctrl Pts',(-0.0498806325786677,-0.145400296738327,
0.24));
#24080=CARTESIAN_POINT('Ctrl Pts',(-0.0594363948008725,-0.140639648297949,
0.24));
#24081=CARTESIAN_POINT('Ctrl Pts',(-0.0684062055177017,-0.134931499399492,
0.24));
#24082=CARTESIAN_POINT('Ctrl Pts',(-0.0735915624001909,-0.131631676235849,
0.24));
#24083=CARTESIAN_POINT('Ctrl Pts',(-0.0785806353345173,-0.128014298080738,
0.24));
#24084=CARTESIAN_POINT('Ctrl Pts',(-0.0833462611484583,-0.124102693747304,
0.24));
#24085=CARTESIAN_POINT('Ctrl Pts',(-0.0858656342542594,-0.122034803580736,
0.24));
#24086=CARTESIAN_POINT('Ctrl Pts',(-0.0883241156266364,-0.11988309220465,
0.24));
#24087=CARTESIAN_POINT('Ctrl Pts',(-0.0907117892851122,-0.117655751751618,
0.24));
#24088=CARTESIAN_POINT('Ctrl Pts',(-0.0983819858496404,-0.110500611839494,
0.24));
#24089=CARTESIAN_POINT('Ctrl Pts',(-0.105284458416918,-0.102606966330569,
0.24));
#24090=CARTESIAN_POINT('Ctrl Pts',(-0.111294422020379,-0.0941015332659665,
0.24));
#24091=CARTESIAN_POINT('Ctrl Pts',(-0.114410577497229,-0.0896914812962706,
0.24));
#24092=CARTESIAN_POINT('Ctrl Pts',(-0.117286101138547,-0.0851164738413172,
0.24));
#24093=CARTESIAN_POINT('Ctrl Pts',(-0.119898298320422,-0.0803922539627851,
0.24));
#24094=CARTESIAN_POINT('Ctrl Pts',(-0.1222721977331,-0.0760990011896685,
0.24));
#24095=CARTESIAN_POINT('Ctrl Pts',(-0.124430744329062,-0.0716759619599862,
0.24));
#24096=CARTESIAN_POINT('Ctrl Pts',(-0.126341093034125,-0.0671690272221462,
0.24));
#24097=CARTESIAN_POINT('Ctrl Pts',(-0.129206708925078,-0.060408406100978,
0.24));
#24098=CARTESIAN_POINT('Ctrl Pts',(-0.131522065955468,-0.0534490321795157,
0.24));
#24099=CARTESIAN_POINT('Ctrl Pts',(-0.133233091500091,-0.0463330844490581,
0.24));
#24100=CARTESIAN_POINT('Ctrl Pts',(-0.135004134506116,-0.0389675313754268,
0.24));
#24101=CARTESIAN_POINT('Ctrl Pts',(-0.136127599829873,-0.0314337185245799,
0.24));
#24102=CARTESIAN_POINT('Ctrl Pts',(-0.136615064298196,-0.0238138180582873,
0.24));
#24103=CARTESIAN_POINT('Ctrl Pts',(-0.136813484749433,-0.0207121682209076,
0.24));
#24104=CARTESIAN_POINT('Ctrl Pts',(-0.136906013213758,-0.0175970392000076,
0.24));
#24105=CARTESIAN_POINT('Ctrl Pts',(-0.136893785357156,-0.0144871321155608,
0.24));
#24106=CARTESIAN_POINT('Ctrl Pts',(-0.136861203984761,-0.00620072149302863,
0.24));
#24107=CARTESIAN_POINT('Ctrl Pts',(-0.136088646936857,0.00207357465703332,
0.24));
#24108=CARTESIAN_POINT('Ctrl Pts',(-0.134599584032292,0.0102285531249486,
0.24));
#24109=CARTESIAN_POINT('Ctrl Pts',(-0.133676409755049,0.0152843948425598,
0.24));
#24110=CARTESIAN_POINT('Ctrl Pts',(-0.132477333465274,0.0202942984003417,
0.24));
#24111=CARTESIAN_POINT('Ctrl Pts',(-0.131003622030167,0.0252303138624672,
0.24));
#24112=CARTESIAN_POINT('Ctrl Pts',(-0.129740734874544,0.029460199292259,
0.24));
#24113=CARTESIAN_POINT('Ctrl Pts',(-0.128274507607502,0.0336384499732856,
0.24));
#24114=CARTESIAN_POINT('Ctrl Pts',(-0.126614574688298,0.0377237273426867,
0.24));
#24115=CARTESIAN_POINT('Ctrl Pts',(-0.124573382985647,0.042747324485064,
0.24));
#24116=CARTESIAN_POINT('Ctrl Pts',(-0.122237651925267,0.0476379767326878,
0.24));
#24117=CARTESIAN_POINT('Ctrl Pts',(-0.119609691052418,0.0523617558795304,
0.24));
#24118=CARTESIAN_POINT('Ctrl Pts',(-0.117006563775536,0.0570408964535612,
0.24));
#24119=CARTESIAN_POINT('Ctrl Pts',(-0.114113358229268,0.0615597689541448,
0.24));
#24120=CARTESIAN_POINT('Ctrl Pts',(-0.110947628485839,0.0658586917144141,
0.24));
#24121=CARTESIAN_POINT('Ctrl Pts',(-0.108265305855902,0.0695011687224882,
0.24));
#24122=CARTESIAN_POINT('Ctrl Pts',(-0.105385772272888,0.0729892759232728,
0.24));
#24123=CARTESIAN_POINT('Ctrl Pts',(-0.102309360287629,0.0763011815833395,
0.24));
#24124=CARTESIAN_POINT('Ctrl Pts',(-0.100282916666232,0.0784827457339379,
0.24));
#24125=CARTESIAN_POINT('Ctrl Pts',(-0.0981709975111385,0.0805877996091198,
0.24));
#24126=CARTESIAN_POINT('Ctrl Pts',(-0.0959791030802606,0.0826138105732947,
0.24));
#24127=CARTESIAN_POINT('Origin',(0.,0.,0.24));
#24128=CARTESIAN_POINT('',(0.158771324027147,-0.275,0.24));
#24129=CARTESIAN_POINT('',(0.317542648054294,0.,0.24));
#24130=CARTESIAN_POINT('',(0.158771324027147,-0.275,0.24));
#24131=CARTESIAN_POINT('',(0.158771324027147,0.275,0.24));
#24132=CARTESIAN_POINT('',(0.317542648054294,0.,0.24));
#24133=CARTESIAN_POINT('',(-0.158771324027147,0.275,0.24));
#24134=CARTESIAN_POINT('',(0.158771324027147,0.275,0.24));
#24135=CARTESIAN_POINT('',(-0.317542648054294,5.55111512312578E-17,0.24));
#24136=CARTESIAN_POINT('',(-0.158771324027147,0.275,0.24));
#24137=CARTESIAN_POINT('',(-0.158771324027147,-0.275,0.24));
#24138=CARTESIAN_POINT('',(-0.317542648054294,3.88877587532466E-17,0.24));
#24139=CARTESIAN_POINT('',(-0.158771324027147,-0.275,0.24));
#24140=CARTESIAN_POINT('Origin',(0.,0.,0.12));
#24141=CARTESIAN_POINT('Origin',(-0.158771324027147,-0.275,0.));
#24142=CARTESIAN_POINT('',(-0.158771324027147,-0.275,0.));
#24143=CARTESIAN_POINT('',(0.158771324027147,-0.275,0.));
#24144=CARTESIAN_POINT('',(-0.158771324027147,-0.275,0.));
#24145=CARTESIAN_POINT('',(0.158771324027147,-0.275,0.));
#24146=CARTESIAN_POINT('',(-0.158771324027147,-0.275,0.));
#24147=CARTESIAN_POINT('Origin',(-0.317542648054294,3.88877587532466E-17,
0.));
#24148=CARTESIAN_POINT('',(-0.317542648054294,3.88877587532466E-17,0.));
#24149=CARTESIAN_POINT('',(-0.317542648054294,3.88877587532466E-17,0.));
#24150=CARTESIAN_POINT('',(-0.317542648054294,3.88877587532466E-17,0.));
#24151=CARTESIAN_POINT('Origin',(-0.158771324027147,0.275,0.));
#24152=CARTESIAN_POINT('',(-0.158771324027147,0.275,0.));
#24153=CARTESIAN_POINT('',(-0.158771324027147,0.275,0.));
#24154=CARTESIAN_POINT('',(-0.158771324027147,0.275,0.));
#24155=CARTESIAN_POINT('Origin',(0.158771324027147,0.275,0.));
#24156=CARTESIAN_POINT('',(0.158771324027147,0.275,0.));
#24157=CARTESIAN_POINT('',(0.158771324027147,0.275,0.));
#24158=CARTESIAN_POINT('',(0.158771324027147,0.275,0.));
#24159=CARTESIAN_POINT('Origin',(0.317542648054294,0.,0.));
#24160=CARTESIAN_POINT('',(0.317542648054294,0.,0.));
#24161=CARTESIAN_POINT('',(0.317542648054294,0.,0.));
#24162=CARTESIAN_POINT('',(0.317542648054294,0.,0.));
#24163=CARTESIAN_POINT('Origin',(0.158771324027147,-0.275,0.));
#24164=CARTESIAN_POINT('',(0.158771324027147,-0.275,0.));
#24165=CARTESIAN_POINT('Origin',(0.,0.,0.));
#24793=UNCERTAINTY_MEASURE_WITH_UNIT(LENGTH_MEASURE(0.001),#24810,
'DISTANCE_ACCURACY_VALUE',
'Maximum model space distance between geometric entities at asserted c
onnectivities');
#24796=UNCERTAINTY_MEASURE_WITH_UNIT(LENGTH_MEASURE(0.001),#24810,
'DISTANCE_ACCURACY_VALUE',
'Maximum model space distance between geometric entities at asserted c
onnectivities');
#24806=(
GEOMETRIC_REPRESENTATION_CONTEXT(3)
GLOBAL_UNCERTAINTY_ASSIGNED_CONTEXT((#24793))
GLOBAL_UNIT_ASSIGNED_CONTEXT((#24810,#24812,#24813))
REPRESENTATION_CONTEXT('','3D')
);
#24809=(
GEOMETRIC_REPRESENTATION_CONTEXT(3)
GLOBAL_UNCERTAINTY_ASSIGNED_CONTEXT((#24796))
GLOBAL_UNIT_ASSIGNED_CONTEXT((#24810,#24812,#24813))
REPRESENTATION_CONTEXT('','3D')
);
#24810=(
LENGTH_UNIT()
NAMED_UNIT(*)
SI_UNIT(.CENTI.,.METRE.)
);
#24812=(
NAMED_UNIT(*)
PLANE_ANGLE_UNIT()
SI_UNIT($,.RADIAN.)
);
#24813=(
NAMED_UNIT(*)
SI_UNIT($,.STERADIAN.)
SOLID_ANGLE_UNIT()
);
#24823=SHAPE_DEFINITION_REPRESENTATION(#24835,#24863);
#24835=PRODUCT_DEFINITION_SHAPE('',$,#24876);
#24863=SHAPE_REPRESENTATION('',(#10569),#24806);
#24866=PRODUCT_DEFINITION_CONTEXT('part definition',#24904,'design');
#24876=PRODUCT_DEFINITION('2026-11-10-05-11-11-303','Hex nut M3',#24888,
#24866);
#24888=PRODUCT_DEFINITION_FORMATION('',$,#24915);
#24904=APPLICATION_CONTEXT(
'Core Data for Automotive Mechanical Design Process');
#24905=PRODUCT_CONTEXT('part definition',#24904,'mechanical');
#24915=PRODUCT('2026-11-10-05-11-11-303','Hex nut M3',$,(#24905));
#24923=PRESENTATION_STYLE_ASSIGNMENT((#24931));
#24931=SURFACE_STYLE_USAGE(.BOTH.,#24939);
#24939=SURFACE_SIDE_STYLE('',(#24947));
#24947=SURFACE_STYLE_FILL_AREA(#24955);
#24955=FILL_AREA_STYLE('Fastener gray',(#24963));
#24963=FILL_AREA_STYLE_COLOUR('Fastener gray',#24971);
#24971=COLOUR_RGB('Fastener gray',0.607843137254902,0.643137254901961,0.698039215686274);
ENDSEC;
END-ISO-10303-21;
